ISO-10303-21;
HEADER;
/* Generated by software containing ST-Developer
 * from STEP Tools, Inc. (www.steptools.com) 
 */

FILE_DESCRIPTION(
/* description */ (''),
/* implementation_level */ '2;1');

FILE_NAME(
/* name */ 'ISO 4026 - M2 x 2 - 45H (Pinion Set Screw).step',
/* time_stamp */ '2026-10-05T09:57:53+05:00',
/* author */ (''),
/* organization */ (''),
/* preprocessor_version */ 'ST-DEVELOPER v20.2',
/* originating_system */ 'Autodesk Translation Framework v15.15.0.0',
/* authorisation */ '');

FILE_SCHEMA (('AUTOMOTIVE_DESIGN { 1 0 10303 214 3 1 1 }'));
ENDSEC;

DATA;
#10=MECHANICAL_DESIGN_GEOMETRIC_PRESENTATION_REPRESENTATION('',(#563),#113984);
#395=(
BOUNDED_CURVE()
B_SPLINE_CURVE(2,(#106350,#106351,#106352),.UNSPECIFIED.,.F.,.F.)
B_SPLINE_CURVE_WITH_KNOTS((3,3),(0.,0.0160544451505013),.UNSPECIFIED.)
CURVE()
GEOMETRIC_REPRESENTATION_ITEM()
RATIONAL_B_SPLINE_CURVE((1.,1.02110226650162,1.02586827095084))
REPRESENTATION_ITEM('')
);
#396=(
BOUNDED_CURVE()
B_SPLINE_CURVE(2,(#106356,#106357,#106358),.UNSPECIFIED.,.F.,.F.)
B_SPLINE_CURVE_WITH_KNOTS((3,3),(0.0254220173370198,0.0414764624875277),
 .UNSPECIFIED.)
CURVE()
GEOMETRIC_REPRESENTATION_ITEM()
RATIONAL_B_SPLINE_CURVE((1.02586827094927,1.02110226650035,1.))
REPRESENTATION_ITEM('')
);
#397=(
BOUNDED_CURVE()
B_SPLINE_CURVE(2,(#106360,#106361,#106362),.UNSPECIFIED.,.F.,.F.)
B_SPLINE_CURVE_WITH_KNOTS((3,3),(0.,0.0160544451505076),.UNSPECIFIED.)
CURVE()
GEOMETRIC_REPRESENTATION_ITEM()
RATIONAL_B_SPLINE_CURVE((1.,1.02110226650074,1.02586827094974))
REPRESENTATION_ITEM('')
);
#398=(
BOUNDED_CURVE()
B_SPLINE_CURVE(2,(#106366,#106367,#106368),.UNSPECIFIED.,.F.,.F.)
B_SPLINE_CURVE_WITH_KNOTS((3,3),(0.0254220173370225,0.0414764624875298),
 .UNSPECIFIED.)
CURVE()
GEOMETRIC_REPRESENTATION_ITEM()
RATIONAL_B_SPLINE_CURVE((1.02586827094974,1.02110226650074,1.))
REPRESENTATION_ITEM('')
);
#399=(
BOUNDED_CURVE()
B_SPLINE_CURVE(2,(#106370,#106371,#106372),.UNSPECIFIED.,.F.,.F.)
B_SPLINE_CURVE_WITH_KNOTS((3,3),(0.,0.0160544451505037),.UNSPECIFIED.)
CURVE()
GEOMETRIC_REPRESENTATION_ITEM()
RATIONAL_B_SPLINE_CURVE((1.,1.02110226650177,1.02586827095102))
REPRESENTATION_ITEM('')
);
#400=(
BOUNDED_CURVE()
B_SPLINE_CURVE(2,(#106376,#106377,#106378),.UNSPECIFIED.,.F.,.F.)
B_SPLINE_CURVE_WITH_KNOTS((3,3),(0.0254220173370244,0.0414764624875264),
 .UNSPECIFIED.)
CURVE()
GEOMETRIC_REPRESENTATION_ITEM()
RATIONAL_B_SPLINE_CURVE((1.02586827094965,1.02110226650066,1.))
REPRESENTATION_ITEM('')
);
#401=(
BOUNDED_CURVE()
B_SPLINE_CURVE(2,(#106380,#106381,#106382),.UNSPECIFIED.,.F.,.F.)
B_SPLINE_CURVE_WITH_KNOTS((3,3),(0.,0.0160544451505027),.UNSPECIFIED.)
CURVE()
GEOMETRIC_REPRESENTATION_ITEM()
RATIONAL_B_SPLINE_CURVE((1.,1.02110226650163,1.02586827095084))
REPRESENTATION_ITEM('')
);
#402=(
BOUNDED_CURVE()
B_SPLINE_CURVE(2,(#106386,#106387,#106388),.UNSPECIFIED.,.F.,.F.)
B_SPLINE_CURVE_WITH_KNOTS((3,3),(0.0254220173370205,0.0414764624875277),
 .UNSPECIFIED.)
CURVE()
GEOMETRIC_REPRESENTATION_ITEM()
RATIONAL_B_SPLINE_CURVE((1.02586827094927,1.02110226650035,1.))
REPRESENTATION_ITEM('')
);
#403=(
BOUNDED_CURVE()
B_SPLINE_CURVE(2,(#106390,#106391,#106392),.UNSPECIFIED.,.F.,.F.)
B_SPLINE_CURVE_WITH_KNOTS((3,3),(0.,0.0160544451505042),.UNSPECIFIED.)
CURVE()
GEOMETRIC_REPRESENTATION_ITEM()
RATIONAL_B_SPLINE_CURVE((1.,1.02110226650138,1.02586827095053))
REPRESENTATION_ITEM('')
);
#404=(
BOUNDED_CURVE()
B_SPLINE_CURVE(2,(#106396,#106397,#106398),.UNSPECIFIED.,.F.,.F.)
B_SPLINE_CURVE_WITH_KNOTS((3,3),(0.0254220173370228,0.0414764624875268),
 .UNSPECIFIED.)
CURVE()
GEOMETRIC_REPRESENTATION_ITEM()
RATIONAL_B_SPLINE_CURVE((1.02586827095053,1.02110226650138,1.))
REPRESENTATION_ITEM('')
);
#405=(
BOUNDED_CURVE()
B_SPLINE_CURVE(2,(#106400,#106401,#106402),.UNSPECIFIED.,.F.,.F.)
B_SPLINE_CURVE_WITH_KNOTS((3,3),(0.,0.0160544451505048),.UNSPECIFIED.)
CURVE()
GEOMETRIC_REPRESENTATION_ITEM()
RATIONAL_B_SPLINE_CURVE((1.,1.02110226650167,1.02586827095089))
REPRESENTATION_ITEM('')
);
#406=(
BOUNDED_CURVE()
B_SPLINE_CURVE(2,(#106405,#106406,#106407),.UNSPECIFIED.,.F.,.F.)
B_SPLINE_CURVE_WITH_KNOTS((3,3),(0.0254220173370243,0.0414764624875262),
 .UNSPECIFIED.)
CURVE()
GEOMETRIC_REPRESENTATION_ITEM()
RATIONAL_B_SPLINE_CURVE((1.02586827094985,1.02110226650082,1.))
REPRESENTATION_ITEM('')
);
#527=SHAPE_REPRESENTATION_RELATIONSHIP('SRR','None',#114064,#545);
#545=ADVANCED_BREP_SHAPE_REPRESENTATION('',(#581),#113978);
#563=STYLED_ITEM('',(#114317),#581);
#581=MANIFOLD_SOLID_BREP('ISO 4026 - M2 x 2 - 45H (Pinion Set Screw)',#60404);
#759=CYLINDRICAL_SURFACE('',#63189,0.96675);
#760=CYLINDRICAL_SURFACE('',#63191,0.96675);
#761=CYLINDRICAL_SURFACE('',#63192,0.96675);
#762=CYLINDRICAL_SURFACE('',#63193,0.96675);
#763=CYLINDRICAL_SURFACE('',#63195,0.739000000000001);
#764=CYLINDRICAL_SURFACE('',#63197,0.739000000000001);
#765=CYLINDRICAL_SURFACE('',#63198,0.739000000000001);
#766=CYLINDRICAL_SURFACE('',#63205,0.739000000000001);
#767=CYLINDRICAL_SURFACE('',#63214,0.469615242270667);
#768=CYLINDRICAL_SURFACE('',#63216,0.469615242270667);
#769=CYLINDRICAL_SURFACE('',#63218,0.469615242270667);
#770=CYLINDRICAL_SURFACE('',#63220,0.469615242270667);
#771=CYLINDRICAL_SURFACE('',#63222,0.469615242270667);
#772=CYLINDRICAL_SURFACE('',#63224,0.469615242270667);
#773=CYLINDRICAL_SURFACE('',#63254,0.96675);
#937=CONICAL_SURFACE('',#63206,0.569615242270665,0.785398163397437);
#938=CONICAL_SURFACE('',#63247,0.519615242270657,1.02974425867665);
#939=CONICAL_SURFACE('',#63253,0.88000000000001,0.785398163397439);
#940=CONICAL_SURFACE('',#63256,0.749999999999993,0.785398163397439);
#1332=CIRCLE('',#63190,0.96675);
#1333=CIRCLE('',#63194,0.96675);
#1334=CIRCLE('',#63196,0.739000000000001);
#1335=CIRCLE('',#63200,0.96675);
#1336=CIRCLE('',#63202,0.96675);
#1337=CIRCLE('',#63203,0.96675);
#1338=CIRCLE('',#63204,0.739000000000001);
#1339=CIRCLE('',#63207,0.669615242270665);
#1340=CIRCLE('',#63208,0.469615242270667);
#1341=CIRCLE('',#63209,0.469615242270667);
#1342=CIRCLE('',#63210,0.469615242270667);
#1343=CIRCLE('',#63211,0.469615242270667);
#1344=CIRCLE('',#63212,0.469615242270667);
#1345=CIRCLE('',#63213,0.469615242270667);
#1346=CIRCLE('',#63215,0.469615242270667);
#1347=CIRCLE('',#63217,0.469615242270667);
#1348=CIRCLE('',#63219,0.469615242270667);
#1349=CIRCLE('',#63221,0.469615242270667);
#1350=CIRCLE('',#63223,0.469615242270667);
#1351=CIRCLE('',#63225,0.469615242270667);
#1352=CIRCLE('',#63236,0.519615242270657);
#1353=CIRCLE('',#63238,0.519615242270657);
#1354=CIRCLE('',#63240,0.519615242270657);
#1355=CIRCLE('',#63242,0.519615242270657);
#1356=CIRCLE('',#63244,0.519615242270657);
#1357=CIRCLE('',#63246,0.519615242270657);
#1358=CIRCLE('',#63252,0.760000000000005);
#1359=CIRCLE('',#63255,0.96675);
#1360=CIRCLE('',#63257,0.500000000000007);
#1853=FACE_BOUND('',#10551,.T.);
#3815=PLANE('',#63199);
#3816=PLANE('',#63201);
#3817=PLANE('',#63226);
#3818=PLANE('',#63227);
#3819=PLANE('',#63228);
#3820=PLANE('',#63229);
#3821=PLANE('',#63230);
#3822=PLANE('',#63231);
#3823=PLANE('',#63232);
#3824=PLANE('',#63233);
#3825=PLANE('',#63234);
#3826=PLANE('',#63235);
#3827=PLANE('',#63237);
#3828=PLANE('',#63239);
#3829=PLANE('',#63241);
#3830=PLANE('',#63243);
#3831=PLANE('',#63245);
#3832=PLANE('',#63248);
#3833=PLANE('',#63249);
#3834=PLANE('',#63250);
#3835=PLANE('',#63251);
#3836=PLANE('',#63258);
#6934=FACE_OUTER_BOUND('',#10512,.T.);
#6935=FACE_OUTER_BOUND('',#10513,.T.);
#6936=FACE_OUTER_BOUND('',#10514,.T.);
#6937=FACE_OUTER_BOUND('',#10515,.T.);
#6938=FACE_OUTER_BOUND('',#10516,.T.);
#6939=FACE_OUTER_BOUND('',#10517,.T.);
#6940=FACE_OUTER_BOUND('',#10518,.T.);
#6941=FACE_OUTER_BOUND('',#10519,.T.);
#6942=FACE_OUTER_BOUND('',#10520,.T.);
#6943=FACE_OUTER_BOUND('',#10521,.T.);
#6944=FACE_OUTER_BOUND('',#10522,.T.);
#6945=FACE_OUTER_BOUND('',#10523,.T.);
#6946=FACE_OUTER_BOUND('',#10524,.T.);
#6947=FACE_OUTER_BOUND('',#10525,.T.);
#6948=FACE_OUTER_BOUND('',#10526,.T.);
#6949=FACE_OUTER_BOUND('',#10527,.T.);
#6950=FACE_OUTER_BOUND('',#10528,.T.);
#6951=FACE_OUTER_BOUND('',#10529,.T.);
#6952=FACE_OUTER_BOUND('',#10530,.T.);
#6953=FACE_OUTER_BOUND('',#10531,.T.);
#6954=FACE_OUTER_BOUND('',#10532,.T.);
#6955=FACE_OUTER_BOUND('',#10533,.T.);
#6956=FACE_OUTER_BOUND('',#10534,.T.);
#6957=FACE_OUTER_BOUND('',#10535,.T.);
#6958=FACE_OUTER_BOUND('',#10536,.T.);
#6959=FACE_OUTER_BOUND('',#10537,.T.);
#6960=FACE_OUTER_BOUND('',#10538,.T.);
#6961=FACE_OUTER_BOUND('',#10539,.T.);
#6962=FACE_OUTER_BOUND('',#10540,.T.);
#6963=FACE_OUTER_BOUND('',#10541,.T.);
#6964=FACE_OUTER_BOUND('',#10542,.T.);
#6965=FACE_OUTER_BOUND('',#10543,.T.);
#6966=FACE_OUTER_BOUND('',#10544,.T.);
#6967=FACE_OUTER_BOUND('',#10545,.T.);
#6968=FACE_OUTER_BOUND('',#10546,.T.);
#6969=FACE_OUTER_BOUND('',#10547,.T.);
#6970=FACE_OUTER_BOUND('',#10548,.T.);
#6971=FACE_OUTER_BOUND('',#10549,.T.);
#6972=FACE_OUTER_BOUND('',#10550,.T.);
#6973=FACE_OUTER_BOUND('',#10552,.T.);
#6974=FACE_OUTER_BOUND('',#10553,.T.);
#6975=FACE_OUTER_BOUND('',#10554,.T.);
#6976=FACE_OUTER_BOUND('',#10555,.T.);
#10512=EDGE_LOOP('',(#54519,#54520,#54521,#54522));
#10513=EDGE_LOOP('',(#54523,#54524,#54525,#54526));
#10514=EDGE_LOOP('',(#54527,#54528,#54529,#54530));
#10515=EDGE_LOOP('',(#54531,#54532,#54533,#54534,#54535));
#10516=EDGE_LOOP('',(#54536,#54537,#54538,#54539));
#10517=EDGE_LOOP('',(#54540,#54541,#54542,#54543));
#10518=EDGE_LOOP('',(#54544,#54545,#54546,#54547));
#10519=EDGE_LOOP('',(#54548,#54549,#54550,#54551));
#10520=EDGE_LOOP('',(#54552,#54553,#54554,#54555,#54556,#54557,#54558,#54559,
#54560,#54561,#54562));
#10521=EDGE_LOOP('',(#54563,#54564,#54565,#54566,#54567));
#10522=EDGE_LOOP('',(#54568,#54569,#54570,#54571));
#10523=EDGE_LOOP('',(#54572,#54573,#54574,#54575,#54576,#54577,#54578,#54579,
#54580,#54581));
#10524=EDGE_LOOP('',(#54582,#54583,#54584,#54585,#54586,#54587,#54588,#54589,
#54590,#54591,#54592,#54593,#54594,#54595,#54596,#54597,#54598,#54599,#54600,
#54601,#54602));
#10525=EDGE_LOOP('',(#54603,#54604,#54605,#54606));
#10526=EDGE_LOOP('',(#54607,#54608,#54609,#54610));
#10527=EDGE_LOOP('',(#54611,#54612,#54613,#54614));
#10528=EDGE_LOOP('',(#54615,#54616,#54617,#54618));
#10529=EDGE_LOOP('',(#54619,#54620,#54621,#54622));
#10530=EDGE_LOOP('',(#54623,#54624,#54625,#54626));
#10531=EDGE_LOOP('',(#54627,#54628,#54629,#54630,#54631,#54632,#54633,#54634));
#10532=EDGE_LOOP('',(#54635,#54636,#54637,#54638,#54639,#54640,#54641,#54642));
#10533=EDGE_LOOP('',(#54643,#54644,#54645,#54646,#54647,#54648,#54649,#54650));
#10534=EDGE_LOOP('',(#54651,#54652));
#10535=EDGE_LOOP('',(#54653,#54654));
#10536=EDGE_LOOP('',(#54655,#54656));
#10537=EDGE_LOOP('',(#54657,#54658));
#10538=EDGE_LOOP('',(#54659,#54660));
#10539=EDGE_LOOP('',(#54661,#54662));
#10540=EDGE_LOOP('',(#54663,#54664));
#10541=EDGE_LOOP('',(#54665,#54666));
#10542=EDGE_LOOP('',(#54667,#54668));
#10543=EDGE_LOOP('',(#54669,#54670));
#10544=EDGE_LOOP('',(#54671,#54672));
#10545=EDGE_LOOP('',(#54673,#54674));
#10546=EDGE_LOOP('',(#54675,#54676,#54677,#54678,#54679,#54680,#54681,#54682));
#10547=EDGE_LOOP('',(#54683,#54684,#54685,#54686,#54687,#54688,#54689,#54690));
#10548=EDGE_LOOP('',(#54691,#54692,#54693,#54694,#54695,#54696,#54697,#54698));
#10549=EDGE_LOOP('',(#54699,#54700,#54701,#54702,#54703,#54704,#54705,#54706));
#10550=EDGE_LOOP('',(#54707));
#10551=EDGE_LOOP('',(#54708));
#10552=EDGE_LOOP('',(#54709,#54710,#54711,#54712,#54713,#54714));
#10553=EDGE_LOOP('',(#54715,#54716,#54717));
#10554=EDGE_LOOP('',(#54718,#54719,#54720,#54721,#54722,#54723));
#10555=EDGE_LOOP('',(#54724));
#16490=LINE('',#105566,#22524);
#16491=LINE('',#105590,#22525);
#16492=LINE('',#105638,#22526);
#16493=LINE('',#105686,#22527);
#16494=LINE('',#105739,#22528);
#16495=LINE('',#105760,#22529);
#16496=LINE('',#105785,#22530);
#16497=LINE('',#106348,#22531);
#16498=LINE('',#106410,#22532);
#16499=LINE('',#106412,#22533);
#16500=LINE('',#106416,#22534);
#16501=LINE('',#106418,#22535);
#16502=LINE('',#106422,#22536);
#16503=LINE('',#106425,#22537);
#16504=LINE('',#106428,#22538);
#16505=LINE('',#106430,#22539);
#16506=LINE('',#106434,#22540);
#16507=LINE('',#106437,#22541);
#16508=LINE('',#106440,#22542);
#16509=LINE('',#106443,#22543);
#16510=LINE('',#106445,#22544);
#16511=LINE('',#106447,#22545);
#16512=LINE('',#106449,#22546);
#16513=LINE('',#106450,#22547);
#16514=LINE('',#106452,#22548);
#16515=LINE('',#106454,#22549);
#16516=LINE('',#106455,#22550);
#16517=LINE('',#106457,#22551);
#16518=LINE('',#106459,#22552);
#16519=LINE('',#106460,#22553);
#16520=LINE('',#106464,#22554);
#16521=LINE('',#106467,#22555);
#16522=LINE('',#106469,#22556);
#16523=LINE('',#106472,#22557);
#16524=LINE('',#106482,#22558);
#16525=LINE('',#106485,#22559);
#16526=LINE('',#106489,#22560);
#16527=LINE('',#106491,#22561);
#16528=LINE('',#106493,#22562);
#16529=LINE('',#106499,#22563);
#16530=LINE('',#106505,#22564);
#22524=VECTOR('',#74552,0.999999999999996);
#22525=VECTOR('',#74557,0.999999999999996);
#22526=VECTOR('',#74560,0.999999999999996);
#22527=VECTOR('',#74563,0.999999999999996);
#22528=VECTOR('',#74568,0.739000000000001);
#22529=VECTOR('',#74573,0.739000000000001);
#22530=VECTOR('',#74576,0.739000000000001);
#22531=VECTOR('',#74595,0.569615242270665);
#22532=VECTOR('',#74610,10.);
#22533=VECTOR('',#74611,10.);
#22534=VECTOR('',#74616,10.);
#22535=VECTOR('',#74617,10.);
#22536=VECTOR('',#74622,10.);
#22537=VECTOR('',#74625,10.);
#22538=VECTOR('',#74628,10.);
#22539=VECTOR('',#74629,10.);
#22540=VECTOR('',#74634,10.);
#22541=VECTOR('',#74637,10.);
#22542=VECTOR('',#74640,10.);
#22543=VECTOR('',#74643,10.);
#22544=VECTOR('',#74646,10.);
#22545=VECTOR('',#74647,10.);
#22546=VECTOR('',#74648,10.);
#22547=VECTOR('',#74649,10.);
#22548=VECTOR('',#74652,10.);
#22549=VECTOR('',#74653,10.);
#22550=VECTOR('',#74654,10.);
#22551=VECTOR('',#74657,10.);
#22552=VECTOR('',#74658,10.);
#22553=VECTOR('',#74659,10.);
#22554=VECTOR('',#74666,10.);
#22555=VECTOR('',#74671,10.);
#22556=VECTOR('',#74674,10.);
#22557=VECTOR('',#74677,10.);
#22558=VECTOR('',#74694,10.);
#22559=VECTOR('',#74699,10.);
#22560=VECTOR('',#74704,0.519615242270657);
#22561=VECTOR('',#74707,10.);
#22562=VECTOR('',#74710,10.);
#22563=VECTOR('',#74719,0.88000000000001);
#22564=VECTOR('',#74728,0.749999999999993);
#24426=B_SPLINE_CURVE_WITH_KNOTS('',3,(#105568,#105569,#105570,#105571,
#105572,#105573,#105574,#105575,#105576,#105577),.UNSPECIFIED.,.F.,.F.,
(4,3,3,4),(-4.09157007060749,-3.98296996538366,-2.98722747403775,-2.06546402602184),
 .UNSPECIFIED.);
#24427=B_SPLINE_CURVE_WITH_KNOTS('',3,(#105580,#105581,#105582,#105583,
#105584,#105585,#105586),.UNSPECIFIED.,.F.,.F.,(4,3,4),(0.,0.995742491345911,
1.11548660900407),.UNSPECIFIED.);
#24428=B_SPLINE_CURVE_WITH_KNOTS('',3,(#105591,#105592,#105593,#105594,
#105595,#105596,#105597,#105598,#105599,#105600,#105601,#105602,#105603,
#105604,#105605,#105606,#105607,#105608,#105609,#105610,#105611,#105612),
 .UNSPECIFIED.,.F.,.F.,(4,3,3,3,3,3,3,4),(-10.3747553777871,-9.95742491345914,
-8.96168242211323,-7.96593993076731,-6.9701974394214,-5.97445494807549,
-4.97871245672958,-4.09157007060749),.UNSPECIFIED.);
#24429=B_SPLINE_CURVE_WITH_KNOTS('',3,(#105613,#105614,#105615,#105616,
#105617,#105618,#105619,#105620,#105621,#105622,#105623,#105624,#105625,
#105626,#105627,#105628,#105629,#105630,#105631,#105632,#105633,#105634),
 .UNSPECIFIED.,.F.,.F.,(4,3,3,3,3,3,3,4),(1.11548660900407,1.99148498269182,
2.98722747403774,3.98296996538365,4.97871245672956,5.97445494807547,6.97019743942139,
7.39867191618366),.UNSPECIFIED.);
#24430=B_SPLINE_CURVE_WITH_KNOTS('',3,(#105639,#105640,#105641,#105642,
#105643,#105644,#105645,#105646,#105647,#105648,#105649,#105650,#105651,
#105652,#105653,#105654,#105655,#105656,#105657,#105658,#105659,#105660),
 .UNSPECIFIED.,.F.,.F.,(4,3,3,3,3,3,3,4),(-16.6579406849667,-15.9318798615346,
-14.9361373701887,-13.9403948788428,-12.9446523874969,-11.948909896151,
-10.9531674048051,-10.3747553777871),.UNSPECIFIED.);
#24431=B_SPLINE_CURVE_WITH_KNOTS('',3,(#105661,#105662,#105663,#105664,
#105665,#105666,#105667,#105668,#105669,#105670,#105671,#105672,#105673,
#105674,#105675,#105676,#105677,#105678,#105679,#105680,#105681,#105682),
 .UNSPECIFIED.,.F.,.F.,(4,3,3,3,3,3,3,4),(7.39867191618366,7.9659399307673,
8.96168242211322,9.95742491345913,10.953167404805,11.948909896151,12.9446523874969,
13.6818572233633),.UNSPECIFIED.);
#24432=B_SPLINE_CURVE_WITH_KNOTS('',3,(#105689,#105690,#105691,#105692,
#105693,#105694,#105695,#105696,#105697,#105698,#105699,#105700,#105701,
#105702,#105703,#105704,#105705,#105706,#105707,#105708,#105709,#105710),
 .UNSPECIFIED.,.F.,.F.,(4,3,3,3,3,3,3,4),(-22.902077300956,-21.9063348096101,
-20.9105923182642,-19.9148498269183,-18.9191073355724,-17.9233648442264,
-16.9276223528805,-16.6579406849667),.UNSPECIFIED.);
#24433=B_SPLINE_CURVE_WITH_KNOTS('',3,(#105711,#105712,#105713,#105714,
#105715,#105716,#105717,#105718,#105719,#105720,#105721,#105722,#105723,
#105724,#105725,#105726,#105727,#105728,#105729,#105730,#105731,#105732,
#105733,#105734,#105735),.UNSPECIFIED.,.F.,.F.,(4,3,3,3,3,3,3,3,4),(13.6818572233633,
13.9403948788428,14.9361373701887,15.9318798615346,16.9276223528805,17.9233648442264,
18.9191073355724,19.9148498269183,19.9650425305428),.UNSPECIFIED.);
#24434=B_SPLINE_CURVE_WITH_KNOTS('',3,(#105741,#105742,#105743,#105744,
#105745,#105746,#105747,#105748),.UNSPECIFIED.,.F.,.F.,(4,1,1,1,1,4),(28.2743338823082,
28.544015550222,29.5397580415679,30.5355005329138,31.5312430242597,32.4530064722757),
 .UNSPECIFIED.);
#24435=B_SPLINE_CURVE_WITH_KNOTS('',3,(#105751,#105752,#105753,#105754,
#105755,#105756),.UNSPECIFIED.,.F.,.F.,(4,1,1,4),(28.2743338823082,29.2198836700295,
30.2156261613754,31.2113686527213),.UNSPECIFIED.);
#24436=B_SPLINE_CURVE_WITH_KNOTS('',3,(#105761,#105762,#105763,#105764,
#105765,#105766,#105767,#105768,#105769,#105770),.UNSPECIFIED.,.F.,.F.,
(4,1,1,1,1,1,1,4),(21.9911485751286,22.5695606021465,23.5653030934924,24.5610455848383,
25.5567880761843,26.5525305675302,27.5482730588761,28.2743338823082),
 .UNSPECIFIED.);
#24437=B_SPLINE_CURVE_WITH_KNOTS('',3,(#105771,#105772,#105773,#105774,
#105775,#105776,#105777,#105778,#105779,#105780,#105781),.UNSPECIFIED.,
 .F.,.F.,(4,1,1,1,1,1,1,1,4),(21.9911485751286,22.2496862306081,23.245428721954,
24.2411712132999,25.2369137046458,26.2326561959917,27.2283986873376,28.2241411786836,
28.2743338823082),.UNSPECIFIED.);
#24438=B_SPLINE_CURVE_WITH_KNOTS('',3,(#105786,#105787,#105788,#105789,
#105790,#105791,#105792,#105793,#105794,#105795),.UNSPECIFIED.,.F.,.F.,
(4,1,1,1,1,1,1,4),(15.707963267949,16.595105654071,17.590848145417,18.5865906367629,
19.5823331281088,20.5780756194547,21.5738181108006,21.9911485751286),
 .UNSPECIFIED.);
#24439=B_SPLINE_CURVE_WITH_KNOTS('',3,(#105796,#105797,#105798,#105799,
#105800,#105801,#105802,#105803,#105804,#105805),.UNSPECIFIED.,.F.,.F.,
(4,1,1,1,1,1,1,4),(15.707963267949,16.2752312825326,17.2709737738785,18.2667162652244,
19.2624587565703,20.2582012479163,21.2539437392622,21.9911485751286),
 .UNSPECIFIED.);
#24440=B_SPLINE_CURVE_WITH_KNOTS('',3,(#105807,#105808,#105809,#105810,
#105811,#105812,#105813,#105814,#105815,#105816,#105817,#105818,#105819,
#105820,#105821,#105822,#105823,#105824,#105825,#105826,#105827,#105828,
#105829,#105830,#105831,#105832,#105833,#105834,#105835,#105836,#105837,
#105838,#105839,#105840,#105841,#105842,#105843,#105844,#105845,#105846,
#105847,#105848,#105849,#105850,#105851,#105852,#105853,#105854,#105855,
#105856,#105857,#105858,#105859,#105860,#105861,#105862,#105863,#105864,
#105865,#105866,#105867,#105868,#105869,#105870,#105871,#105872,#105873,
#105874,#105875,#105876,#105877,#105878,#105879),.UNSPECIFIED.,.F.,.F.,
(4,3,3,3,3,3,3,3,3,3,3,3,3,3,3,3,3,3,3,3,3,3,3,3,4),(-0.178587760439472,
-0.172997303911014,-0.162856682864992,-0.158716158534057,-0.156203682331329,
-0.145417506956393,-0.137581747775137,-0.135179453906191,-0.123829626631807,
-0.112395948228162,-0.106524699914796,-0.103647422367158,-0.0918723355428386,
-0.0803882935999837,-0.0750511880536326,-0.0723197039144465,-0.0701559845024732,
-0.058210449571605,-0.0459784728235496,-0.0402311637206059,-0.0370748175850279,
-0.0346544230216544,-0.0219633623116217,-0.0093557654079626,0.),
 .UNSPECIFIED.);
#24441=B_SPLINE_CURVE_WITH_KNOTS('',3,(#105882,#105883,#105884,#105885,
#105886,#105887,#105888,#105889,#105890,#105891,#105892,#105893,#105894,
#105895,#105896,#105897,#105898,#105899,#105900,#105901,#105902,#105903,
#105904,#105905,#105906,#105907,#105908,#105909,#105910,#105911,#105912,
#105913,#105914,#105915,#105916,#105917,#105918,#105919,#105920,#105921,
#105922,#105923,#105924,#105925,#105926,#105927,#105928,#105929,#105930,
#105931,#105932,#105933,#105934,#105935,#105936,#105937,#105938,#105939,
#105940,#105941,#105942,#105943,#105944,#105945,#105946,#105947,#105948,
#105949,#105950,#105951,#105952,#105953,#105954,#105955,#105956,#105957),
 .UNSPECIFIED.,.F.,.F.,(4,3,3,3,3,3,3,3,3,3,3,3,3,3,3,3,3,3,3,3,3,3,3,3,
3,4),(-0.177567088092108,-0.170427641780406,-0.159117078668393,-0.152710961416868,
-0.149808705938898,-0.137348063727474,-0.130172447872078,-0.127139016091628,
-0.12464907937053,-0.11270555837298,-0.1010409933116,-0.0954973026492411,
-0.093049358993514,-0.0906377927723942,-0.079943136884305,-0.0699502447737669,
-0.0648815661545737,-0.0614861704592656,-0.0586741810352214,-0.0474857631257267,
-0.0364249809192207,-0.0314310426811734,-0.0291079279156276,-0.0185054507233679,
-0.00828997057237845,0.),.UNSPECIFIED.);
#24442=B_SPLINE_CURVE_WITH_KNOTS('',3,(#106062,#106063,#106064,#106065),
 .UNSPECIFIED.,.F.,.F.,(4,4),(19.9650425305428,20.8366132749342),
 .UNSPECIFIED.);
#24443=B_SPLINE_CURVE_WITH_KNOTS('',3,(#106067,#106068,#106069,#106070,
#106071,#106072,#106073,#106074,#106075,#106076,#106077,#106078,#106079,
#106080,#106081,#106082,#106083,#106084,#106085,#106086,#106087,#106088,
#106089,#106090,#106091,#106092,#106093,#106094,#106095,#106096,#106097,
#106098,#106099,#106100,#106101,#106102,#106103,#106104,#106105,#106106,
#106107,#106108,#106109,#106110,#106111,#106112,#106113,#106114,#106115,
#106116,#106117,#106118,#106119,#106120,#106121,#106122,#106123,#106124,
#106125,#106126,#106127,#106128,#106129,#106130,#106131,#106132,#106133,
#106134,#106135,#106136,#106137,#106138,#106139),.UNSPECIFIED.,.F.,.F.,
(4,3,3,3,3,3,3,3,3,3,3,3,3,3,3,3,3,3,3,3,3,3,3,3,4),(-0.178587760439474,
-0.172997303911017,-0.162856682864998,-0.158716160609124,-0.156203687475286,
-0.145417513860255,-0.137581761131997,-0.135179479570029,-0.123829652805094,
-0.112395973547909,-0.106524733023587,-0.103647430899797,-0.0918723355428663,
-0.080388293600008,-0.0750511865962201,-0.0723196871235457,-0.070155957327666,
-0.0582104228184783,-0.0459784469741407,-0.0402311411023731,-0.0370747430924057,
-0.0346543091754803,-0.021963248077658,-0.00935564841229983,0.),
 .UNSPECIFIED.);
#24444=B_SPLINE_CURVE_WITH_KNOTS('',3,(#106140,#106141,#106142,#106143,
#106144,#106145,#106146,#106147,#106148),.UNSPECIFIED.,.F.,.F.,(4,1,1,1,
1,1,4),(10.3747553777871,11.296518825803,12.2922613171489,13.2880038084949,
14.2837462998408,15.2794887911867,15.707963267949),.UNSPECIFIED.);
#24445=B_SPLINE_CURVE_WITH_KNOTS('',3,(#106154,#106155,#106156,#106157,
#106158,#106159,#106160,#106161,#106162,#106163,#106164,#106165,#106166,
#106167,#106168,#106169,#106170,#106171,#106172,#106173,#106174,#106175,
#106176,#106177,#106178,#106179,#106180,#106181,#106182,#106183,#106184,
#106185,#106186,#106187,#106188,#106189,#106190,#106191,#106192,#106193,
#106194,#106195,#106196,#106197,#106198,#106199,#106200,#106201,#106202,
#106203,#106204,#106205,#106206,#106207,#106208,#106209,#106210,#106211,
#106212,#106213,#106214,#106215,#106216,#106217,#106218,#106219,#106220,
#106221,#106222,#106223,#106224,#106225,#106226,#106227,#106228,#106229),
 .UNSPECIFIED.,.F.,.F.,(4,3,3,3,3,3,3,3,3,3,3,3,3,3,3,3,3,3,3,3,3,3,3,3,
3,4),(-0.177567088092073,-0.170427641780375,-0.159117078668367,-0.15271096033015,
-0.149808704260947,-0.137348061616469,-0.13017244602495,-0.127139026932459,
-0.124649081110899,-0.112705557810677,-0.101040988585173,-0.0954972972813229,
-0.0930493469528739,-0.0906377909408365,-0.079943136884317,-0.0699502447737774,
-0.06488156611803,-0.061486171730566,-0.058674181915544,-0.047485764632209,
-0.0364249872579639,-0.0314310514931735,-0.0291079329386753,-0.0185054606443194,
-0.00828998776203388,0.),.UNSPECIFIED.);
#24446=B_SPLINE_CURVE_WITH_KNOTS('',3,(#106232,#106233,#106234,#106235,
#106236,#106237,#106238,#106239),.UNSPECIFIED.,.F.,.F.,(4,1,1,1,1,4),(11.6163931973415,
12.6121356886874,13.6078781800333,14.6036206713792,15.5993631627251,15.707963267949),
 .UNSPECIFIED.);
#29745=VERTEX_POINT('',#105564);
#29746=VERTEX_POINT('',#105565);
#29747=VERTEX_POINT('',#105567);
#29748=VERTEX_POINT('',#105578);
#29749=VERTEX_POINT('',#105588);
#29750=VERTEX_POINT('',#105589);
#29751=VERTEX_POINT('',#105636);
#29752=VERTEX_POINT('',#105637);
#29753=VERTEX_POINT('',#105684);
#29754=VERTEX_POINT('',#105685);
#29755=VERTEX_POINT('',#105687);
#29756=VERTEX_POINT('',#105737);
#29757=VERTEX_POINT('',#105738);
#29758=VERTEX_POINT('',#105740);
#29759=VERTEX_POINT('',#105749);
#29760=VERTEX_POINT('',#105758);
#29761=VERTEX_POINT('',#105759);
#29762=VERTEX_POINT('',#105783);
#29763=VERTEX_POINT('',#105784);
#29764=VERTEX_POINT('',#105880);
#29765=VERTEX_POINT('',#106066);
#29766=VERTEX_POINT('',#106150);
#29767=VERTEX_POINT('',#106153);
#29768=VERTEX_POINT('',#106345);
#29769=VERTEX_POINT('',#106347);
#29770=VERTEX_POINT('',#106349);
#29771=VERTEX_POINT('',#106353);
#29772=VERTEX_POINT('',#106355);
#29773=VERTEX_POINT('',#106359);
#29774=VERTEX_POINT('',#106363);
#29775=VERTEX_POINT('',#106365);
#29776=VERTEX_POINT('',#106369);
#29777=VERTEX_POINT('',#106373);
#29778=VERTEX_POINT('',#106375);
#29779=VERTEX_POINT('',#106379);
#29780=VERTEX_POINT('',#106383);
#29781=VERTEX_POINT('',#106385);
#29782=VERTEX_POINT('',#106389);
#29783=VERTEX_POINT('',#106393);
#29784=VERTEX_POINT('',#106395);
#29785=VERTEX_POINT('',#106399);
#29786=VERTEX_POINT('',#106403);
#29787=VERTEX_POINT('',#106409);
#29788=VERTEX_POINT('',#106411);
#29789=VERTEX_POINT('',#106415);
#29790=VERTEX_POINT('',#106417);
#29791=VERTEX_POINT('',#106421);
#29792=VERTEX_POINT('',#106423);
#29793=VERTEX_POINT('',#106427);
#29794=VERTEX_POINT('',#106429);
#29795=VERTEX_POINT('',#106433);
#29796=VERTEX_POINT('',#106435);
#29797=VERTEX_POINT('',#106439);
#29798=VERTEX_POINT('',#106441);
#29799=VERTEX_POINT('',#106446);
#29800=VERTEX_POINT('',#106448);
#29801=VERTEX_POINT('',#106453);
#29802=VERTEX_POINT('',#106458);
#29803=VERTEX_POINT('',#106471);
#29804=VERTEX_POINT('',#106481);
#29805=VERTEX_POINT('',#106488);
#29806=VERTEX_POINT('',#106496);
#29807=VERTEX_POINT('',#106503);
#38092=EDGE_CURVE('',#29745,#29746,#16490,.T.);
#38093=EDGE_CURVE('',#29745,#29747,#24426,.T.);
#38094=EDGE_CURVE('',#29747,#29748,#1332,.T.);
#38095=EDGE_CURVE('',#29748,#29746,#24427,.T.);
#38096=EDGE_CURVE('',#29749,#29750,#16491,.T.);
#38097=EDGE_CURVE('',#29749,#29745,#24428,.T.);
#38098=EDGE_CURVE('',#29746,#29750,#24429,.T.);
#38099=EDGE_CURVE('',#29751,#29752,#16492,.T.);
#38100=EDGE_CURVE('',#29751,#29749,#24430,.T.);
#38101=EDGE_CURVE('',#29750,#29752,#24431,.T.);
#38102=EDGE_CURVE('',#29753,#29754,#16493,.T.);
#38103=EDGE_CURVE('',#29755,#29753,#1333,.F.);
#38104=EDGE_CURVE('',#29755,#29751,#24432,.T.);
#38105=EDGE_CURVE('',#29752,#29754,#24433,.T.);
#38106=EDGE_CURVE('',#29756,#29757,#16494,.T.);
#38107=EDGE_CURVE('',#29756,#29758,#24434,.T.);
#38108=EDGE_CURVE('',#29759,#29758,#1334,.T.);
#38109=EDGE_CURVE('',#29757,#29759,#24435,.T.);
#38110=EDGE_CURVE('',#29760,#29761,#16495,.T.);
#38111=EDGE_CURVE('',#29760,#29756,#24436,.T.);
#38112=EDGE_CURVE('',#29761,#29757,#24437,.T.);
#38113=EDGE_CURVE('',#29762,#29763,#16496,.T.);
#38114=EDGE_CURVE('',#29762,#29760,#24438,.T.);
#38115=EDGE_CURVE('',#29763,#29761,#24439,.T.);
#38116=EDGE_CURVE('',#29758,#29755,#24440,.T.);
#38117=EDGE_CURVE('',#29764,#29755,#1335,.F.);
#38118=EDGE_CURVE('',#29764,#29759,#24441,.T.);
#38119=EDGE_CURVE('',#29754,#29764,#24442,.T.);
#38120=EDGE_CURVE('',#29765,#29748,#24443,.T.);
#38121=EDGE_CURVE('',#29765,#29763,#24444,.T.);
#38122=EDGE_CURVE('',#29748,#29766,#1336,.T.);
#38123=EDGE_CURVE('',#29766,#29747,#1337,.T.);
#38124=EDGE_CURVE('',#29747,#29767,#24445,.T.);
#38125=EDGE_CURVE('',#29767,#29765,#1338,.T.);
#38126=EDGE_CURVE('',#29767,#29762,#24446,.T.);
#38127=EDGE_CURVE('',#29768,#29768,#1339,.T.);
#38128=EDGE_CURVE('',#29768,#29769,#16497,.T.);
#38129=EDGE_CURVE('',#29770,#29769,#395,.T.);
#38130=EDGE_CURVE('',#29770,#29771,#1340,.T.);
#38131=EDGE_CURVE('',#29772,#29771,#396,.T.);
#38132=EDGE_CURVE('',#29773,#29772,#397,.T.);
#38133=EDGE_CURVE('',#29773,#29774,#1341,.T.);
#38134=EDGE_CURVE('',#29775,#29774,#398,.T.);
#38135=EDGE_CURVE('',#29776,#29775,#399,.T.);
#38136=EDGE_CURVE('',#29776,#29777,#1342,.T.);
#38137=EDGE_CURVE('',#29778,#29777,#400,.T.);
#38138=EDGE_CURVE('',#29779,#29778,#401,.T.);
#38139=EDGE_CURVE('',#29779,#29780,#1343,.T.);
#38140=EDGE_CURVE('',#29781,#29780,#402,.T.);
#38141=EDGE_CURVE('',#29782,#29781,#403,.T.);
#38142=EDGE_CURVE('',#29782,#29783,#1344,.T.);
#38143=EDGE_CURVE('',#29784,#29783,#404,.T.);
#38144=EDGE_CURVE('',#29785,#29784,#405,.T.);
#38145=EDGE_CURVE('',#29785,#29786,#1345,.T.);
#38146=EDGE_CURVE('',#29769,#29786,#406,.T.);
#38147=EDGE_CURVE('',#29774,#29787,#16498,.T.);
#38148=EDGE_CURVE('',#29788,#29773,#16499,.T.);
#38149=EDGE_CURVE('',#29787,#29788,#1346,.T.);
#38150=EDGE_CURVE('',#29777,#29789,#16500,.T.);
#38151=EDGE_CURVE('',#29790,#29776,#16501,.T.);
#38152=EDGE_CURVE('',#29789,#29790,#1347,.T.);
#38153=EDGE_CURVE('',#29791,#29770,#16502,.T.);
#38154=EDGE_CURVE('',#29792,#29791,#1348,.T.);
#38155=EDGE_CURVE('',#29771,#29792,#16503,.T.);
#38156=EDGE_CURVE('',#29780,#29793,#16504,.T.);
#38157=EDGE_CURVE('',#29794,#29779,#16505,.T.);
#38158=EDGE_CURVE('',#29793,#29794,#1349,.T.);
#38159=EDGE_CURVE('',#29795,#29785,#16506,.T.);
#38160=EDGE_CURVE('',#29796,#29795,#1350,.T.);
#38161=EDGE_CURVE('',#29786,#29796,#16507,.T.);
#38162=EDGE_CURVE('',#29797,#29782,#16508,.T.);
#38163=EDGE_CURVE('',#29798,#29797,#1351,.T.);
#38164=EDGE_CURVE('',#29783,#29798,#16509,.T.);
#38165=EDGE_CURVE('',#29794,#29793,#16510,.T.);
#38166=EDGE_CURVE('',#29778,#29799,#16511,.T.);
#38167=EDGE_CURVE('',#29799,#29800,#16512,.T.);
#38168=EDGE_CURVE('',#29781,#29800,#16513,.T.);
#38169=EDGE_CURVE('',#29790,#29789,#16514,.T.);
#38170=EDGE_CURVE('',#29775,#29801,#16515,.T.);
#38171=EDGE_CURVE('',#29801,#29799,#16516,.T.);
#38172=EDGE_CURVE('',#29788,#29787,#16517,.T.);
#38173=EDGE_CURVE('',#29772,#29802,#16518,.T.);
#38174=EDGE_CURVE('',#29802,#29801,#16519,.T.);
#38175=EDGE_CURVE('',#29791,#29792,#16520,.T.);
#38176=EDGE_CURVE('',#29795,#29796,#16521,.T.);
#38177=EDGE_CURVE('',#29797,#29798,#16522,.T.);
#38178=EDGE_CURVE('',#29803,#29802,#16523,.T.);
#38179=EDGE_CURVE('',#29803,#29802,#1352,.T.);
#38180=EDGE_CURVE('',#29802,#29801,#1353,.T.);
#38181=EDGE_CURVE('',#29801,#29799,#1354,.T.);
#38182=EDGE_CURVE('',#29799,#29800,#1355,.T.);
#38183=EDGE_CURVE('',#29800,#29804,#16524,.T.);
#38184=EDGE_CURVE('',#29800,#29804,#1356,.T.);
#38185=EDGE_CURVE('',#29804,#29803,#16525,.T.);
#38186=EDGE_CURVE('',#29804,#29803,#1357,.T.);
#38187=EDGE_CURVE('',#29803,#29805,#16526,.T.);
#38188=EDGE_CURVE('',#29769,#29803,#16527,.T.);
#38189=EDGE_CURVE('',#29784,#29804,#16528,.T.);
#38190=EDGE_CURVE('',#29806,#29806,#1358,.T.);
#38191=EDGE_CURVE('',#29766,#29806,#16529,.T.);
#38192=EDGE_CURVE('',#29753,#29764,#1359,.F.);
#38193=EDGE_CURVE('',#29807,#29807,#1360,.T.);
#38194=EDGE_CURVE('',#29807,#29753,#16530,.T.);
#54519=ORIENTED_EDGE('',*,*,#38092,.F.);
#54520=ORIENTED_EDGE('',*,*,#38093,.T.);
#54521=ORIENTED_EDGE('',*,*,#38094,.T.);
#54522=ORIENTED_EDGE('',*,*,#38095,.T.);
#54523=ORIENTED_EDGE('',*,*,#38096,.F.);
#54524=ORIENTED_EDGE('',*,*,#38097,.T.);
#54525=ORIENTED_EDGE('',*,*,#38092,.T.);
#54526=ORIENTED_EDGE('',*,*,#38098,.T.);
#54527=ORIENTED_EDGE('',*,*,#38099,.F.);
#54528=ORIENTED_EDGE('',*,*,#38100,.T.);
#54529=ORIENTED_EDGE('',*,*,#38096,.T.);
#54530=ORIENTED_EDGE('',*,*,#38101,.T.);
#54531=ORIENTED_EDGE('',*,*,#38102,.F.);
#54532=ORIENTED_EDGE('',*,*,#38103,.F.);
#54533=ORIENTED_EDGE('',*,*,#38104,.T.);
#54534=ORIENTED_EDGE('',*,*,#38099,.T.);
#54535=ORIENTED_EDGE('',*,*,#38105,.T.);
#54536=ORIENTED_EDGE('',*,*,#38106,.F.);
#54537=ORIENTED_EDGE('',*,*,#38107,.T.);
#54538=ORIENTED_EDGE('',*,*,#38108,.F.);
#54539=ORIENTED_EDGE('',*,*,#38109,.F.);
#54540=ORIENTED_EDGE('',*,*,#38110,.F.);
#54541=ORIENTED_EDGE('',*,*,#38111,.T.);
#54542=ORIENTED_EDGE('',*,*,#38106,.T.);
#54543=ORIENTED_EDGE('',*,*,#38112,.F.);
#54544=ORIENTED_EDGE('',*,*,#38113,.F.);
#54545=ORIENTED_EDGE('',*,*,#38114,.T.);
#54546=ORIENTED_EDGE('',*,*,#38110,.T.);
#54547=ORIENTED_EDGE('',*,*,#38115,.F.);
#54548=ORIENTED_EDGE('',*,*,#38108,.T.);
#54549=ORIENTED_EDGE('',*,*,#38116,.T.);
#54550=ORIENTED_EDGE('',*,*,#38117,.F.);
#54551=ORIENTED_EDGE('',*,*,#38118,.T.);
#54552=ORIENTED_EDGE('',*,*,#38118,.F.);
#54553=ORIENTED_EDGE('',*,*,#38119,.F.);
#54554=ORIENTED_EDGE('',*,*,#38105,.F.);
#54555=ORIENTED_EDGE('',*,*,#38101,.F.);
#54556=ORIENTED_EDGE('',*,*,#38098,.F.);
#54557=ORIENTED_EDGE('',*,*,#38095,.F.);
#54558=ORIENTED_EDGE('',*,*,#38120,.F.);
#54559=ORIENTED_EDGE('',*,*,#38121,.T.);
#54560=ORIENTED_EDGE('',*,*,#38115,.T.);
#54561=ORIENTED_EDGE('',*,*,#38112,.T.);
#54562=ORIENTED_EDGE('',*,*,#38109,.T.);
#54563=ORIENTED_EDGE('',*,*,#38122,.T.);
#54564=ORIENTED_EDGE('',*,*,#38123,.T.);
#54565=ORIENTED_EDGE('',*,*,#38124,.T.);
#54566=ORIENTED_EDGE('',*,*,#38125,.T.);
#54567=ORIENTED_EDGE('',*,*,#38120,.T.);
#54568=ORIENTED_EDGE('',*,*,#38113,.T.);
#54569=ORIENTED_EDGE('',*,*,#38121,.F.);
#54570=ORIENTED_EDGE('',*,*,#38125,.F.);
#54571=ORIENTED_EDGE('',*,*,#38126,.T.);
#54572=ORIENTED_EDGE('',*,*,#38116,.F.);
#54573=ORIENTED_EDGE('',*,*,#38107,.F.);
#54574=ORIENTED_EDGE('',*,*,#38111,.F.);
#54575=ORIENTED_EDGE('',*,*,#38114,.F.);
#54576=ORIENTED_EDGE('',*,*,#38126,.F.);
#54577=ORIENTED_EDGE('',*,*,#38124,.F.);
#54578=ORIENTED_EDGE('',*,*,#38093,.F.);
#54579=ORIENTED_EDGE('',*,*,#38097,.F.);
#54580=ORIENTED_EDGE('',*,*,#38100,.F.);
#54581=ORIENTED_EDGE('',*,*,#38104,.F.);
#54582=ORIENTED_EDGE('',*,*,#38127,.F.);
#54583=ORIENTED_EDGE('',*,*,#38128,.T.);
#54584=ORIENTED_EDGE('',*,*,#38129,.F.);
#54585=ORIENTED_EDGE('',*,*,#38130,.T.);
#54586=ORIENTED_EDGE('',*,*,#38131,.F.);
#54587=ORIENTED_EDGE('',*,*,#38132,.F.);
#54588=ORIENTED_EDGE('',*,*,#38133,.T.);
#54589=ORIENTED_EDGE('',*,*,#38134,.F.);
#54590=ORIENTED_EDGE('',*,*,#38135,.F.);
#54591=ORIENTED_EDGE('',*,*,#38136,.T.);
#54592=ORIENTED_EDGE('',*,*,#38137,.F.);
#54593=ORIENTED_EDGE('',*,*,#38138,.F.);
#54594=ORIENTED_EDGE('',*,*,#38139,.T.);
#54595=ORIENTED_EDGE('',*,*,#38140,.F.);
#54596=ORIENTED_EDGE('',*,*,#38141,.F.);
#54597=ORIENTED_EDGE('',*,*,#38142,.T.);
#54598=ORIENTED_EDGE('',*,*,#38143,.F.);
#54599=ORIENTED_EDGE('',*,*,#38144,.F.);
#54600=ORIENTED_EDGE('',*,*,#38145,.T.);
#54601=ORIENTED_EDGE('',*,*,#38146,.F.);
#54602=ORIENTED_EDGE('',*,*,#38128,.F.);
#54603=ORIENTED_EDGE('',*,*,#38147,.F.);
#54604=ORIENTED_EDGE('',*,*,#38133,.F.);
#54605=ORIENTED_EDGE('',*,*,#38148,.F.);
#54606=ORIENTED_EDGE('',*,*,#38149,.F.);
#54607=ORIENTED_EDGE('',*,*,#38150,.F.);
#54608=ORIENTED_EDGE('',*,*,#38136,.F.);
#54609=ORIENTED_EDGE('',*,*,#38151,.F.);
#54610=ORIENTED_EDGE('',*,*,#38152,.F.);
#54611=ORIENTED_EDGE('',*,*,#38153,.F.);
#54612=ORIENTED_EDGE('',*,*,#38154,.F.);
#54613=ORIENTED_EDGE('',*,*,#38155,.F.);
#54614=ORIENTED_EDGE('',*,*,#38130,.F.);
#54615=ORIENTED_EDGE('',*,*,#38156,.F.);
#54616=ORIENTED_EDGE('',*,*,#38139,.F.);
#54617=ORIENTED_EDGE('',*,*,#38157,.F.);
#54618=ORIENTED_EDGE('',*,*,#38158,.F.);
#54619=ORIENTED_EDGE('',*,*,#38159,.F.);
#54620=ORIENTED_EDGE('',*,*,#38160,.F.);
#54621=ORIENTED_EDGE('',*,*,#38161,.F.);
#54622=ORIENTED_EDGE('',*,*,#38145,.F.);
#54623=ORIENTED_EDGE('',*,*,#38162,.F.);
#54624=ORIENTED_EDGE('',*,*,#38163,.F.);
#54625=ORIENTED_EDGE('',*,*,#38164,.F.);
#54626=ORIENTED_EDGE('',*,*,#38142,.F.);
#54627=ORIENTED_EDGE('',*,*,#38140,.T.);
#54628=ORIENTED_EDGE('',*,*,#38156,.T.);
#54629=ORIENTED_EDGE('',*,*,#38165,.F.);
#54630=ORIENTED_EDGE('',*,*,#38157,.T.);
#54631=ORIENTED_EDGE('',*,*,#38138,.T.);
#54632=ORIENTED_EDGE('',*,*,#38166,.T.);
#54633=ORIENTED_EDGE('',*,*,#38167,.T.);
#54634=ORIENTED_EDGE('',*,*,#38168,.F.);
#54635=ORIENTED_EDGE('',*,*,#38137,.T.);
#54636=ORIENTED_EDGE('',*,*,#38150,.T.);
#54637=ORIENTED_EDGE('',*,*,#38169,.F.);
#54638=ORIENTED_EDGE('',*,*,#38151,.T.);
#54639=ORIENTED_EDGE('',*,*,#38135,.T.);
#54640=ORIENTED_EDGE('',*,*,#38170,.T.);
#54641=ORIENTED_EDGE('',*,*,#38171,.T.);
#54642=ORIENTED_EDGE('',*,*,#38166,.F.);
#54643=ORIENTED_EDGE('',*,*,#38134,.T.);
#54644=ORIENTED_EDGE('',*,*,#38147,.T.);
#54645=ORIENTED_EDGE('',*,*,#38172,.F.);
#54646=ORIENTED_EDGE('',*,*,#38148,.T.);
#54647=ORIENTED_EDGE('',*,*,#38132,.T.);
#54648=ORIENTED_EDGE('',*,*,#38173,.T.);
#54649=ORIENTED_EDGE('',*,*,#38174,.T.);
#54650=ORIENTED_EDGE('',*,*,#38170,.F.);
#54651=ORIENTED_EDGE('',*,*,#38149,.T.);
#54652=ORIENTED_EDGE('',*,*,#38172,.T.);
#54653=ORIENTED_EDGE('',*,*,#38152,.T.);
#54654=ORIENTED_EDGE('',*,*,#38169,.T.);
#54655=ORIENTED_EDGE('',*,*,#38154,.T.);
#54656=ORIENTED_EDGE('',*,*,#38175,.T.);
#54657=ORIENTED_EDGE('',*,*,#38158,.T.);
#54658=ORIENTED_EDGE('',*,*,#38165,.T.);
#54659=ORIENTED_EDGE('',*,*,#38160,.T.);
#54660=ORIENTED_EDGE('',*,*,#38176,.T.);
#54661=ORIENTED_EDGE('',*,*,#38163,.T.);
#54662=ORIENTED_EDGE('',*,*,#38177,.T.);
#54663=ORIENTED_EDGE('',*,*,#38178,.F.);
#54664=ORIENTED_EDGE('',*,*,#38179,.T.);
#54665=ORIENTED_EDGE('',*,*,#38174,.F.);
#54666=ORIENTED_EDGE('',*,*,#38180,.T.);
#54667=ORIENTED_EDGE('',*,*,#38171,.F.);
#54668=ORIENTED_EDGE('',*,*,#38181,.T.);
#54669=ORIENTED_EDGE('',*,*,#38167,.F.);
#54670=ORIENTED_EDGE('',*,*,#38182,.T.);
#54671=ORIENTED_EDGE('',*,*,#38183,.F.);
#54672=ORIENTED_EDGE('',*,*,#38184,.T.);
#54673=ORIENTED_EDGE('',*,*,#38185,.F.);
#54674=ORIENTED_EDGE('',*,*,#38186,.T.);
#54675=ORIENTED_EDGE('',*,*,#38182,.F.);
#54676=ORIENTED_EDGE('',*,*,#38181,.F.);
#54677=ORIENTED_EDGE('',*,*,#38180,.F.);
#54678=ORIENTED_EDGE('',*,*,#38179,.F.);
#54679=ORIENTED_EDGE('',*,*,#38187,.T.);
#54680=ORIENTED_EDGE('',*,*,#38187,.F.);
#54681=ORIENTED_EDGE('',*,*,#38186,.F.);
#54682=ORIENTED_EDGE('',*,*,#38184,.F.);
#54683=ORIENTED_EDGE('',*,*,#38129,.T.);
#54684=ORIENTED_EDGE('',*,*,#38188,.T.);
#54685=ORIENTED_EDGE('',*,*,#38178,.T.);
#54686=ORIENTED_EDGE('',*,*,#38173,.F.);
#54687=ORIENTED_EDGE('',*,*,#38131,.T.);
#54688=ORIENTED_EDGE('',*,*,#38155,.T.);
#54689=ORIENTED_EDGE('',*,*,#38175,.F.);
#54690=ORIENTED_EDGE('',*,*,#38153,.T.);
#54691=ORIENTED_EDGE('',*,*,#38144,.T.);
#54692=ORIENTED_EDGE('',*,*,#38189,.T.);
#54693=ORIENTED_EDGE('',*,*,#38185,.T.);
#54694=ORIENTED_EDGE('',*,*,#38188,.F.);
#54695=ORIENTED_EDGE('',*,*,#38146,.T.);
#54696=ORIENTED_EDGE('',*,*,#38161,.T.);
#54697=ORIENTED_EDGE('',*,*,#38176,.F.);
#54698=ORIENTED_EDGE('',*,*,#38159,.T.);
#54699=ORIENTED_EDGE('',*,*,#38141,.T.);
#54700=ORIENTED_EDGE('',*,*,#38168,.T.);
#54701=ORIENTED_EDGE('',*,*,#38183,.T.);
#54702=ORIENTED_EDGE('',*,*,#38189,.F.);
#54703=ORIENTED_EDGE('',*,*,#38143,.T.);
#54704=ORIENTED_EDGE('',*,*,#38164,.T.);
#54705=ORIENTED_EDGE('',*,*,#38177,.F.);
#54706=ORIENTED_EDGE('',*,*,#38162,.T.);
#54707=ORIENTED_EDGE('',*,*,#38190,.F.);
#54708=ORIENTED_EDGE('',*,*,#38127,.T.);
#54709=ORIENTED_EDGE('',*,*,#38122,.F.);
#54710=ORIENTED_EDGE('',*,*,#38094,.F.);
#54711=ORIENTED_EDGE('',*,*,#38123,.F.);
#54712=ORIENTED_EDGE('',*,*,#38191,.T.);
#54713=ORIENTED_EDGE('',*,*,#38190,.T.);
#54714=ORIENTED_EDGE('',*,*,#38191,.F.);
#54715=ORIENTED_EDGE('',*,*,#38102,.T.);
#54716=ORIENTED_EDGE('',*,*,#38119,.T.);
#54717=ORIENTED_EDGE('',*,*,#38192,.F.);
#54718=ORIENTED_EDGE('',*,*,#38193,.F.);
#54719=ORIENTED_EDGE('',*,*,#38194,.T.);
#54720=ORIENTED_EDGE('',*,*,#38192,.T.);
#54721=ORIENTED_EDGE('',*,*,#38117,.T.);
#54722=ORIENTED_EDGE('',*,*,#38103,.T.);
#54723=ORIENTED_EDGE('',*,*,#38194,.F.);
#54724=ORIENTED_EDGE('',*,*,#38193,.T.);
#57115=B_SPLINE_SURFACE_WITH_KNOTS('',3,3,((#105958,#105959,#105960,#105961,
#105962,#105963,#105964,#105965,#105966,#105967,#105968,#105969,#105970,
#105971,#105972,#105973,#105974,#105975,#105976,#105977,#105978,#105979,
#105980,#105981,#105982,#105983),(#105984,#105985,#105986,#105987,#105988,
#105989,#105990,#105991,#105992,#105993,#105994,#105995,#105996,#105997,
#105998,#105999,#106000,#106001,#106002,#106003,#106004,#106005,#106006,
#106007,#106008,#106009),(#106010,#106011,#106012,#106013,#106014,#106015,
#106016,#106017,#106018,#106019,#106020,#106021,#106022,#106023,#106024,
#106025,#106026,#106027,#106028,#106029,#106030,#106031,#106032,#106033,
#106034,#106035),(#106036,#106037,#106038,#106039,#106040,#106041,#106042,
#106043,#106044,#106045,#106046,#106047,#106048,#106049,#106050,#106051,
#106052,#106053,#106054,#106055,#106056,#106057,#106058,#106059,#106060,
#106061)),.UNSPECIFIED.,.F.,.F.,.F.,(4,4),(4,1,1,1,1,1,1,1,1,1,1,1,1,1,
1,1,1,1,1,1,1,1,1,4),(0.,0.026298304761587),(8.3092913517653,9.30503384311121,
10.3007763344571,11.296518825803,12.2922613171489,13.2880038084949,14.2837462998408,
15.2794887911867,16.2752312825326,17.2709737738785,18.2667162652244,19.2624587565703,
20.2582012479163,21.2539437392622,22.2496862306081,23.245428721954,24.2411712132999,
25.2369137046458,26.2326561959917,27.2283986873376,28.2241411786836,29.2198836700295,
30.2156261613754,31.2113686527213),.UNSPECIFIED.);
#57116=B_SPLINE_SURFACE_WITH_KNOTS('',3,3,((#106240,#106241,#106242,#106243,
#106244,#106245,#106246,#106247,#106248,#106249,#106250,#106251,#106252,
#106253,#106254,#106255,#106256,#106257,#106258,#106259,#106260,#106261,
#106262,#106263,#106264,#106265),(#106266,#106267,#106268,#106269,#106270,
#106271,#106272,#106273,#106274,#106275,#106276,#106277,#106278,#106279,
#106280,#106281,#106282,#106283,#106284,#106285,#106286,#106287,#106288,
#106289,#106290,#106291),(#106292,#106293,#106294,#106295,#106296,#106297,
#106298,#106299,#106300,#106301,#106302,#106303,#106304,#106305,#106306,
#106307,#106308,#106309,#106310,#106311,#106312,#106313,#106314,#106315,
#106316,#106317),(#106318,#106319,#106320,#106321,#106322,#106323,#106324,
#106325,#106326,#106327,#106328,#106329,#106330,#106331,#106332,#106333,
#106334,#106335,#106336,#106337,#106338,#106339,#106340,#106341,#106342,
#106343)),.UNSPECIFIED.,.F.,.F.,.F.,(4,4),(4,1,1,1,1,1,1,1,1,1,1,1,1,1,
1,1,1,1,1,1,1,1,1,4),(0.,0.026298304761587),(11.6163931973415,12.6121356886874,
13.6078781800333,14.6036206713792,15.5993631627251,16.595105654071,17.590848145417,
18.5865906367629,19.5823331281088,20.5780756194547,21.5738181108006,22.5695606021465,
23.5653030934924,24.5610455848383,25.5567880761843,26.5525305675302,27.5482730588761,
28.544015550222,29.5397580415679,30.5355005329138,31.5312430242597,32.5269855156056,
33.5227280069516,34.5184704982975),.UNSPECIFIED.);
#60034=ADVANCED_FACE('',(#6934),#759,.T.);
#60035=ADVANCED_FACE('',(#6935),#760,.T.);
#60036=ADVANCED_FACE('',(#6936),#761,.T.);
#60037=ADVANCED_FACE('',(#6937),#762,.T.);
#60038=ADVANCED_FACE('',(#6938),#763,.T.);
#60039=ADVANCED_FACE('',(#6939),#764,.T.);
#60040=ADVANCED_FACE('',(#6940),#765,.T.);
#60041=ADVANCED_FACE('',(#6941),#3815,.T.);
#60042=ADVANCED_FACE('',(#6942),#57115,.F.);
#60043=ADVANCED_FACE('',(#6943),#3816,.F.);
#60044=ADVANCED_FACE('',(#6944),#766,.T.);
#60045=ADVANCED_FACE('',(#6945),#57116,.F.);
#60046=ADVANCED_FACE('',(#6946),#937,.F.);
#60047=ADVANCED_FACE('',(#6947),#767,.T.);
#60048=ADVANCED_FACE('',(#6948),#768,.T.);
#60049=ADVANCED_FACE('',(#6949),#769,.T.);
#60050=ADVANCED_FACE('',(#6950),#770,.T.);
#60051=ADVANCED_FACE('',(#6951),#771,.T.);
#60052=ADVANCED_FACE('',(#6952),#772,.T.);
#60053=ADVANCED_FACE('',(#6953),#3817,.F.);
#60054=ADVANCED_FACE('',(#6954),#3818,.F.);
#60055=ADVANCED_FACE('',(#6955),#3819,.F.);
#60056=ADVANCED_FACE('',(#6956),#3820,.T.);
#60057=ADVANCED_FACE('',(#6957),#3821,.T.);
#60058=ADVANCED_FACE('',(#6958),#3822,.T.);
#60059=ADVANCED_FACE('',(#6959),#3823,.T.);
#60060=ADVANCED_FACE('',(#6960),#3824,.T.);
#60061=ADVANCED_FACE('',(#6961),#3825,.T.);
#60062=ADVANCED_FACE('',(#6962),#3826,.F.);
#60063=ADVANCED_FACE('',(#6963),#3827,.F.);
#60064=ADVANCED_FACE('',(#6964),#3828,.F.);
#60065=ADVANCED_FACE('',(#6965),#3829,.F.);
#60066=ADVANCED_FACE('',(#6966),#3830,.F.);
#60067=ADVANCED_FACE('',(#6967),#3831,.F.);
#60068=ADVANCED_FACE('',(#6968),#938,.F.);
#60069=ADVANCED_FACE('',(#6969),#3832,.F.);
#60070=ADVANCED_FACE('',(#6970),#3833,.F.);
#60071=ADVANCED_FACE('',(#6971),#3834,.F.);
#60072=ADVANCED_FACE('',(#6972,#1853),#3835,.T.);
#60073=ADVANCED_FACE('',(#6973),#939,.T.);
#60074=ADVANCED_FACE('',(#6974),#773,.T.);
#60075=ADVANCED_FACE('',(#6975),#940,.T.);
#60076=ADVANCED_FACE('',(#6976),#3836,.T.);
#60404=CLOSED_SHELL('',(#60034,#60035,#60036,#60037,#60038,#60039,#60040,
#60041,#60042,#60043,#60044,#60045,#60046,#60047,#60048,#60049,#60050,#60051,
#60052,#60053,#60054,#60055,#60056,#60057,#60058,#60059,#60060,#60061,#60062,
#60063,#60064,#60065,#60066,#60067,#60068,#60069,#60070,#60071,#60072,#60073,
#60074,#60075,#60076));
#63188=AXIS2_PLACEMENT_3D('',#105562,#74548,#74549);
#63189=AXIS2_PLACEMENT_3D('',#105563,#74550,#74551);
#63190=AXIS2_PLACEMENT_3D('',#105579,#74553,#74554);
#63191=AXIS2_PLACEMENT_3D('',#105587,#74555,#74556);
#63192=AXIS2_PLACEMENT_3D('',#105635,#74558,#74559);
#63193=AXIS2_PLACEMENT_3D('',#105683,#74561,#74562);
#63194=AXIS2_PLACEMENT_3D('',#105688,#74564,#74565);
#63195=AXIS2_PLACEMENT_3D('',#105736,#74566,#74567);
#63196=AXIS2_PLACEMENT_3D('',#105750,#74569,#74570);
#63197=AXIS2_PLACEMENT_3D('',#105757,#74571,#74572);
#63198=AXIS2_PLACEMENT_3D('',#105782,#74574,#74575);
#63199=AXIS2_PLACEMENT_3D('',#105806,#74577,#74578);
#63200=AXIS2_PLACEMENT_3D('',#105881,#74579,#74580);
#63201=AXIS2_PLACEMENT_3D('',#106149,#74581,#74582);
#63202=AXIS2_PLACEMENT_3D('',#106151,#74583,#74584);
#63203=AXIS2_PLACEMENT_3D('',#106152,#74585,#74586);
#63204=AXIS2_PLACEMENT_3D('',#106230,#74587,#74588);
#63205=AXIS2_PLACEMENT_3D('',#106231,#74589,#74590);
#63206=AXIS2_PLACEMENT_3D('',#106344,#74591,#74592);
#63207=AXIS2_PLACEMENT_3D('',#106346,#74593,#74594);
#63208=AXIS2_PLACEMENT_3D('',#106354,#74596,#74597);
#63209=AXIS2_PLACEMENT_3D('',#106364,#74598,#74599);
#63210=AXIS2_PLACEMENT_3D('',#106374,#74600,#74601);
#63211=AXIS2_PLACEMENT_3D('',#106384,#74602,#74603);
#63212=AXIS2_PLACEMENT_3D('',#106394,#74604,#74605);
#63213=AXIS2_PLACEMENT_3D('',#106404,#74606,#74607);
#63214=AXIS2_PLACEMENT_3D('',#106408,#74608,#74609);
#63215=AXIS2_PLACEMENT_3D('',#106413,#74612,#74613);
#63216=AXIS2_PLACEMENT_3D('',#106414,#74614,#74615);
#63217=AXIS2_PLACEMENT_3D('',#106419,#74618,#74619);
#63218=AXIS2_PLACEMENT_3D('',#106420,#74620,#74621);
#63219=AXIS2_PLACEMENT_3D('',#106424,#74623,#74624);
#63220=AXIS2_PLACEMENT_3D('',#106426,#74626,#74627);
#63221=AXIS2_PLACEMENT_3D('',#106431,#74630,#74631);
#63222=AXIS2_PLACEMENT_3D('',#106432,#74632,#74633);
#63223=AXIS2_PLACEMENT_3D('',#106436,#74635,#74636);
#63224=AXIS2_PLACEMENT_3D('',#106438,#74638,#74639);
#63225=AXIS2_PLACEMENT_3D('',#106442,#74641,#74642);
#63226=AXIS2_PLACEMENT_3D('',#106444,#74644,#74645);
#63227=AXIS2_PLACEMENT_3D('',#106451,#74650,#74651);
#63228=AXIS2_PLACEMENT_3D('',#106456,#74655,#74656);
#63229=AXIS2_PLACEMENT_3D('',#106461,#74660,#74661);
#63230=AXIS2_PLACEMENT_3D('',#106462,#74662,#74663);
#63231=AXIS2_PLACEMENT_3D('',#106463,#74664,#74665);
#63232=AXIS2_PLACEMENT_3D('',#106465,#74667,#74668);
#63233=AXIS2_PLACEMENT_3D('',#106466,#74669,#74670);
#63234=AXIS2_PLACEMENT_3D('',#106468,#74672,#74673);
#63235=AXIS2_PLACEMENT_3D('',#106470,#74675,#74676);
#63236=AXIS2_PLACEMENT_3D('',#106473,#74678,#74679);
#63237=AXIS2_PLACEMENT_3D('',#106474,#74680,#74681);
#63238=AXIS2_PLACEMENT_3D('',#106475,#74682,#74683);
#63239=AXIS2_PLACEMENT_3D('',#106476,#74684,#74685);
#63240=AXIS2_PLACEMENT_3D('',#106477,#74686,#74687);
#63241=AXIS2_PLACEMENT_3D('',#106478,#74688,#74689);
#63242=AXIS2_PLACEMENT_3D('',#106479,#74690,#74691);
#63243=AXIS2_PLACEMENT_3D('',#106480,#74692,#74693);
#63244=AXIS2_PLACEMENT_3D('',#106483,#74695,#74696);
#63245=AXIS2_PLACEMENT_3D('',#106484,#74697,#74698);
#63246=AXIS2_PLACEMENT_3D('',#106486,#74700,#74701);
#63247=AXIS2_PLACEMENT_3D('',#106487,#74702,#74703);
#63248=AXIS2_PLACEMENT_3D('',#106490,#74705,#74706);
#63249=AXIS2_PLACEMENT_3D('',#106492,#74708,#74709);
#63250=AXIS2_PLACEMENT_3D('',#106494,#74711,#74712);
#63251=AXIS2_PLACEMENT_3D('',#106495,#74713,#74714);
#63252=AXIS2_PLACEMENT_3D('',#106497,#74715,#74716);
#63253=AXIS2_PLACEMENT_3D('',#106498,#74717,#74718);
#63254=AXIS2_PLACEMENT_3D('',#106500,#74720,#74721);
#63255=AXIS2_PLACEMENT_3D('',#106501,#74722,#74723);
#63256=AXIS2_PLACEMENT_3D('',#106502,#74724,#74725);
#63257=AXIS2_PLACEMENT_3D('',#106504,#74726,#74727);
#63258=AXIS2_PLACEMENT_3D('',#106506,#74729,#74730);
#74548=DIRECTION('axis',(0.,0.,1.));
#74549=DIRECTION('refdir',(1.,0.,0.));
#74550=DIRECTION('center_axis',(0.,-1.,0.));
#74551=DIRECTION('ref_axis',(1.,0.,0.));
#74552=DIRECTION('',(0.,1.,0.));
#74553=DIRECTION('center_axis',(0.,-1.,0.));
#74554=DIRECTION('ref_axis',(1.,0.,0.));
#74555=DIRECTION('center_axis',(0.,-1.,0.));
#74556=DIRECTION('ref_axis',(1.,0.,0.));
#74557=DIRECTION('',(0.,1.,0.));
#74558=DIRECTION('center_axis',(0.,-1.,0.));
#74559=DIRECTION('ref_axis',(1.,0.,0.));
#74560=DIRECTION('',(0.,1.,0.));
#74561=DIRECTION('center_axis',(0.,-1.,0.));
#74562=DIRECTION('ref_axis',(1.,0.,0.));
#74563=DIRECTION('',(0.,1.,0.));
#74564=DIRECTION('center_axis',(0.,1.,0.));
#74565=DIRECTION('ref_axis',(1.,0.,0.));
#74566=DIRECTION('center_axis',(0.,-1.,0.));
#74567=DIRECTION('ref_axis',(0.495633595239364,0.,-0.868531714602353));
#74568=DIRECTION('',(0.,-1.,0.));
#74569=DIRECTION('center_axis',(0.,-1.,0.));
#74570=DIRECTION('ref_axis',(1.,0.,0.));
#74571=DIRECTION('center_axis',(0.,-1.,0.));
#74572=DIRECTION('ref_axis',(1.,0.,0.));
#74573=DIRECTION('',(0.,-1.,0.));
#74574=DIRECTION('center_axis',(0.,-1.,0.));
#74575=DIRECTION('ref_axis',(1.,0.,0.));
#74576=DIRECTION('',(0.,-1.,0.));
#74577=DIRECTION('center_axis',(0.,1.,0.));
#74578=DIRECTION('ref_axis',(0.,0.,1.));
#74579=DIRECTION('center_axis',(0.,1.,0.));
#74580=DIRECTION('ref_axis',(1.,0.,0.));
#74581=DIRECTION('center_axis',(0.,1.,0.));
#74582=DIRECTION('ref_axis',(0.,0.,1.));
#74583=DIRECTION('center_axis',(0.,-1.,0.));
#74584=DIRECTION('ref_axis',(1.,0.,0.));
#74585=DIRECTION('center_axis',(0.,-1.,0.));
#74586=DIRECTION('ref_axis',(1.,0.,0.));
#74587=DIRECTION('center_axis',(0.,1.,0.));
#74588=DIRECTION('ref_axis',(1.,0.,0.));
#74589=DIRECTION('center_axis',(0.,-1.,0.));
#74590=DIRECTION('ref_axis',(1.,0.,0.));
#74591=DIRECTION('center_axis',(0.,1.,0.));
#74592=DIRECTION('ref_axis',(1.,0.,0.));
#74593=DIRECTION('center_axis',(0.,-1.,0.));
#74594=DIRECTION('ref_axis',(1.,0.,0.));
#74595=DIRECTION('',(0.70710678118654,-0.707106781186555,8.65956056235484E-17));
#74596=DIRECTION('center_axis',(0.,-1.,0.));
#74597=DIRECTION('ref_axis',(1.,0.,0.));
#74598=DIRECTION('center_axis',(0.,-1.,0.));
#74599=DIRECTION('ref_axis',(1.,0.,0.));
#74600=DIRECTION('center_axis',(0.,-1.,0.));
#74601=DIRECTION('ref_axis',(1.,0.,0.));
#74602=DIRECTION('center_axis',(0.,-1.,0.));
#74603=DIRECTION('ref_axis',(1.,0.,0.));
#74604=DIRECTION('center_axis',(0.,-1.,0.));
#74605=DIRECTION('ref_axis',(1.,0.,0.));
#74606=DIRECTION('center_axis',(0.,-1.,0.));
#74607=DIRECTION('ref_axis',(1.,0.,0.));
#74608=DIRECTION('center_axis',(0.,-1.,0.));
#74609=DIRECTION('ref_axis',(1.,0.,0.));
#74610=DIRECTION('',(0.,1.,0.));
#74611=DIRECTION('',(0.,-1.,0.));
#74612=DIRECTION('center_axis',(0.,1.,0.));
#74613=DIRECTION('ref_axis',(1.,0.,0.));
#74614=DIRECTION('center_axis',(0.,-1.,0.));
#74615=DIRECTION('ref_axis',(1.,0.,0.));
#74616=DIRECTION('',(0.,1.,0.));
#74617=DIRECTION('',(0.,-1.,0.));
#74618=DIRECTION('center_axis',(0.,1.,0.));
#74619=DIRECTION('ref_axis',(1.,0.,0.));
#74620=DIRECTION('center_axis',(0.,-1.,0.));
#74621=DIRECTION('ref_axis',(1.,0.,0.));
#74622=DIRECTION('',(0.,-1.,0.));
#74623=DIRECTION('center_axis',(0.,1.,0.));
#74624=DIRECTION('ref_axis',(1.,0.,0.));
#74625=DIRECTION('',(0.,1.,0.));
#74626=DIRECTION('center_axis',(0.,-1.,0.));
#74627=DIRECTION('ref_axis',(1.,0.,0.));
#74628=DIRECTION('',(0.,1.,0.));
#74629=DIRECTION('',(0.,-1.,0.));
#74630=DIRECTION('center_axis',(0.,1.,0.));
#74631=DIRECTION('ref_axis',(1.,0.,0.));
#74632=DIRECTION('center_axis',(0.,-1.,0.));
#74633=DIRECTION('ref_axis',(1.,0.,0.));
#74634=DIRECTION('',(0.,-1.,0.));
#74635=DIRECTION('center_axis',(0.,1.,0.));
#74636=DIRECTION('ref_axis',(1.,0.,0.));
#74637=DIRECTION('',(0.,1.,0.));
#74638=DIRECTION('center_axis',(0.,-1.,0.));
#74639=DIRECTION('ref_axis',(1.,0.,0.));
#74640=DIRECTION('',(0.,-1.,0.));
#74641=DIRECTION('center_axis',(0.,1.,0.));
#74642=DIRECTION('ref_axis',(1.,0.,0.));
#74643=DIRECTION('',(0.,1.,0.));
#74644=DIRECTION('center_axis',(0.86602540378445,0.,0.499999999999979));
#74645=DIRECTION('ref_axis',(-0.499999999999979,0.,0.86602540378445));
#74646=DIRECTION('',(-0.499999999999979,0.,0.86602540378445));
#74647=DIRECTION('',(0.,-1.,0.));
#74648=DIRECTION('',(-0.499999999999979,0.,0.86602540378445));
#74649=DIRECTION('',(0.,-1.,0.));
#74650=DIRECTION('center_axis',(0.86602540378445,0.,-0.499999999999979));
#74651=DIRECTION('ref_axis',(0.499999999999979,0.,0.86602540378445));
#74652=DIRECTION('',(0.499999999999979,0.,0.86602540378445));
#74653=DIRECTION('',(0.,-1.,0.));
#74654=DIRECTION('',(0.499999999999979,0.,0.86602540378445));
#74655=DIRECTION('center_axis',(0.,0.,-1.));
#74656=DIRECTION('ref_axis',(1.,0.,0.));
#74657=DIRECTION('',(1.,0.,0.));
#74658=DIRECTION('',(0.,-1.,0.));
#74659=DIRECTION('',(1.,0.,0.));
#74660=DIRECTION('center_axis',(0.,1.,0.));
#74661=DIRECTION('ref_axis',(0.,0.,1.));
#74662=DIRECTION('center_axis',(0.,1.,0.));
#74663=DIRECTION('ref_axis',(0.,0.,1.));
#74664=DIRECTION('center_axis',(0.,1.,0.));
#74665=DIRECTION('ref_axis',(0.,0.,1.));
#74666=DIRECTION('',(0.499999999999979,0.,-0.86602540378445));
#74667=DIRECTION('center_axis',(0.,1.,0.));
#74668=DIRECTION('ref_axis',(0.,0.,1.));
#74669=DIRECTION('center_axis',(0.,1.,0.));
#74670=DIRECTION('ref_axis',(0.,0.,1.));
#74671=DIRECTION('',(-0.499999999999979,0.,-0.86602540378445));
#74672=DIRECTION('center_axis',(0.,1.,0.));
#74673=DIRECTION('ref_axis',(0.,0.,1.));
#74674=DIRECTION('',(-1.,0.,0.));
#74675=DIRECTION('center_axis',(0.,1.,0.));
#74676=DIRECTION('ref_axis',(0.,0.,1.));
#74677=DIRECTION('',(0.499999999999979,0.,-0.86602540378445));
#74678=DIRECTION('center_axis',(0.,-1.,0.));
#74679=DIRECTION('ref_axis',(1.,0.,0.));
#74680=DIRECTION('center_axis',(0.,1.,0.));
#74681=DIRECTION('ref_axis',(0.,0.,1.));
#74682=DIRECTION('center_axis',(0.,-1.,0.));
#74683=DIRECTION('ref_axis',(1.,0.,0.));
#74684=DIRECTION('center_axis',(0.,1.,0.));
#74685=DIRECTION('ref_axis',(0.,0.,1.));
#74686=DIRECTION('center_axis',(0.,-1.,0.));
#74687=DIRECTION('ref_axis',(1.,0.,0.));
#74688=DIRECTION('center_axis',(0.,1.,0.));
#74689=DIRECTION('ref_axis',(0.,0.,1.));
#74690=DIRECTION('center_axis',(0.,-1.,0.));
#74691=DIRECTION('ref_axis',(1.,0.,0.));
#74692=DIRECTION('center_axis',(0.,1.,0.));
#74693=DIRECTION('ref_axis',(0.,0.,1.));
#74694=DIRECTION('',(-1.,0.,0.));
#74695=DIRECTION('center_axis',(0.,-1.,0.));
#74696=DIRECTION('ref_axis',(1.,0.,0.));
#74697=DIRECTION('center_axis',(0.,1.,0.));
#74698=DIRECTION('ref_axis',(0.,0.,1.));
#74699=DIRECTION('',(-0.499999999999979,0.,-0.86602540378445));
#74700=DIRECTION('center_axis',(0.,-1.,0.));
#74701=DIRECTION('ref_axis',(1.,0.,0.));
#74702=DIRECTION('center_axis',(0.,1.,0.));
#74703=DIRECTION('ref_axis',(1.,0.,0.));
#74704=DIRECTION('',(0.857167300702112,-0.515038074910054,1.04972719113862E-16));
#74705=DIRECTION('center_axis',(-0.86602540378445,0.,-0.499999999999979));
#74706=DIRECTION('ref_axis',(0.499999999999979,0.,-0.86602540378445));
#74707=DIRECTION('',(0.,-1.,0.));
#74708=DIRECTION('center_axis',(-0.86602540378445,0.,0.499999999999979));
#74709=DIRECTION('ref_axis',(-0.499999999999979,0.,-0.86602540378445));
#74710=DIRECTION('',(0.,-1.,0.));
#74711=DIRECTION('center_axis',(0.,0.,1.));
#74712=DIRECTION('ref_axis',(-1.,0.,0.));
#74713=DIRECTION('center_axis',(0.,1.,0.));
#74714=DIRECTION('ref_axis',(0.,0.,1.));
#74715=DIRECTION('center_axis',(0.,-1.,0.));
#74716=DIRECTION('ref_axis',(1.,0.,0.));
#74717=DIRECTION('center_axis',(0.,-1.,0.));
#74718=DIRECTION('ref_axis',(1.,0.,0.));
#74719=DIRECTION('',(0.707106781186541,0.707106781186554,8.65956056235485E-17));
#74720=DIRECTION('center_axis',(0.,-1.,0.));
#74721=DIRECTION('ref_axis',(-0.906528546186737,0.,-0.422144519031766));
#74722=DIRECTION('center_axis',(0.,1.,0.));
#74723=DIRECTION('ref_axis',(1.,0.,0.));
#74724=DIRECTION('center_axis',(0.,1.,0.));
#74725=DIRECTION('ref_axis',(1.,0.,0.));
#74726=DIRECTION('center_axis',(0.,-1.,0.));
#74727=DIRECTION('ref_axis',(1.,0.,0.));
#74728=DIRECTION('',(-0.707106781186541,0.707106781186554,-8.65956056235486E-17));
#74729=DIRECTION('center_axis',(0.,-1.,0.));
#74730=DIRECTION('ref_axis',(0.,0.,-1.));
#105562=CARTESIAN_POINT('',(0.,0.,0.));
#105563=CARTESIAN_POINT('Origin',(110.,21.33,33.3));
#105564=CARTESIAN_POINT('',(109.032067739078,21.8642640831103,33.3006146958441));
#105565=CARTESIAN_POINT('',(109.032510608047,21.9222359168897,33.3005483021895));
#105566=CARTESIAN_POINT('',(109.03325,21.33,33.3));
#105567=CARTESIAN_POINT('',(110.425646877672,21.99325,34.1689059799454));
#105568=CARTESIAN_POINT('Ctrl Pts',(109.032067739078,21.8642640831103,33.3006146958441));
#105569=CARTESIAN_POINT('Ctrl Pts',(109.031818204458,21.8665686489192,33.3354978137518));
#105570=CARTESIAN_POINT('Ctrl Pts',(109.033539730099,21.8688732147281,33.3703553556597));
#105571=CARTESIAN_POINT('Ctrl Pts',(109.037313868836,21.871177780537,33.4049881195007));
#105572=CARTESIAN_POINT('Ctrl Pts',(109.071918534281,21.8923080924762,33.7225321446948));
#105573=CARTESIAN_POINT('Ctrl Pts',(109.27908341892,21.9134384044155,34.0211794023689));
#105574=CARTESIAN_POINT('Ctrl Pts',(109.564445284039,21.9345687163547,34.1649116522973));
#105575=CARTESIAN_POINT('Ctrl Pts',(109.828606087672,21.9541291442365,34.2979652634834));
#105576=CARTESIAN_POINT('Ctrl Pts',(110.1597761584,21.9736895721183,34.2982676985065));
#105577=CARTESIAN_POINT('Ctrl Pts',(110.426174626828,21.99325,34.1695497362104));
#105578=CARTESIAN_POINT('',(109.574880871485,21.99325,34.1682622236805));
#105579=CARTESIAN_POINT('Origin',(110.,21.99325,33.3));
#105580=CARTESIAN_POINT('Ctrl Pts',(109.574880871485,21.99325,34.1682622236805));
#105581=CARTESIAN_POINT('Ctrl Pts',(109.286692341569,21.9721196880608,34.0271591636317));
#105582=CARTESIAN_POINT('Ctrl Pts',(109.076879953927,21.9509893761215,33.7321151931956));
#105583=CARTESIAN_POINT('Ctrl Pts',(109.038873374224,21.9298590641823,33.4154564405219));
#105584=CARTESIAN_POINT('Ctrl Pts',(109.034302850829,21.9273180150847,33.3773762910182));
#105585=CARTESIAN_POINT('Ctrl Pts',(109.032216902585,21.9247769659872,33.3389835586544));
#105586=CARTESIAN_POINT('Ctrl Pts',(109.032510608047,21.9222359168897,33.3005483021895));
#105587=CARTESIAN_POINT('Origin',(110.,21.33,33.3));
#105588=CARTESIAN_POINT('',(109.034572229009,21.4642640831103,33.3004087423462));
#105589=CARTESIAN_POINT('',(109.034617182386,21.5222359168897,33.300357734449));
#105590=CARTESIAN_POINT('',(109.03325,21.33,33.3));
#105591=CARTESIAN_POINT('Ctrl Pts',(109.034572229009,21.4642640831103,33.3004087423462));
#105592=CARTESIAN_POINT('Ctrl Pts',(109.034056633714,21.4731201106171,33.4353604451549));
#105593=CARTESIAN_POINT('Ctrl Pts',(109.06044141107,21.4819761381238,33.5701194095229));
#105594=CARTESIAN_POINT('Ctrl Pts',(109.114708801304,21.4908321656306,33.6925157712021));
#105595=CARTESIAN_POINT('Ctrl Pts',(109.244189754576,21.5119624775698,33.9845511449109));
#105596=CARTESIAN_POINT('Ctrl Pts',(109.532403761939,21.5330927895091,34.2062074013583));
#105597=CARTESIAN_POINT('Ctrl Pts',(109.847891962672,21.5542231014483,34.256384606394));
#105598=CARTESIAN_POINT('Ctrl Pts',(110.163380163405,21.5753534133876,34.3065618114296));
#105599=CARTESIAN_POINT('Ctrl Pts',(110.506142557508,21.5964837253268,34.1852599650534));
#105600=CARTESIAN_POINT('Ctrl Pts',(110.719835444608,21.6176140372661,33.947802969508));
#105601=CARTESIAN_POINT('Ctrl Pts',(110.933528331708,21.6387443492053,33.7103459739625));
#105602=CARTESIAN_POINT('Ctrl Pts',(111.018151711806,21.6598746611446,33.3567338292479));
#105603=CARTESIAN_POINT('Ctrl Pts',(110.935113419845,21.6810049730838,33.0482654179561));
#105604=CARTESIAN_POINT('Ctrl Pts',(110.852075127883,21.702135285023,32.7397970066643));
#105605=CARTESIAN_POINT('Ctrl Pts',(110.601375163861,21.7232655969623,32.4764723287954));
#105606=CARTESIAN_POINT('Ctrl Pts',(110.297349367024,21.7443959089015,32.3783791328529));
#105607=CARTESIAN_POINT('Ctrl Pts',(109.993323570188,21.7655262208408,32.2802859369104));
#105608=CARTESIAN_POINT('Ctrl Pts',(109.635971940536,21.78665653278,32.3474242228943));
#105609=CARTESIAN_POINT('Ctrl Pts',(109.388318348837,21.8077868447193,32.5492137622433));
#105610=CARTESIAN_POINT('Ctrl Pts',(109.167674959425,21.8266125908496,32.7289952368599));
#105611=CARTESIAN_POINT('Ctrl Pts',(109.034106160108,21.84543833698,33.0156583194923));
#105612=CARTESIAN_POINT('Ctrl Pts',(109.032067739078,21.8642640831103,33.3006146958441));
#105613=CARTESIAN_POINT('Ctrl Pts',(109.032510608047,21.9222359168897,33.3005483021895));
#105614=CARTESIAN_POINT('Ctrl Pts',(109.034659235571,21.903646654048,33.0193718835565));
#105615=CARTESIAN_POINT('Ctrl Pts',(109.164161685767,21.8850573912062,32.7359196687374));
#105616=CARTESIAN_POINT('Ctrl Pts',(109.37993974096,21.8664681283645,32.5559234520905));
#105617=CARTESIAN_POINT('Ctrl Pts',(109.625213459164,21.8453378164253,32.3513227512442));
#105618=CARTESIAN_POINT('Ctrl Pts',(109.981961667339,21.8242075044861,32.2803948844628));
#105619=CARTESIAN_POINT('Ctrl Pts',(110.287104459141,21.8030771925468,32.3751482824717));
#105620=CARTESIAN_POINT('Ctrl Pts',(110.592247250944,21.7819468806076,32.4699016804807));
#105621=CARTESIAN_POINT('Ctrl Pts',(110.845784626375,21.7608165686683,32.7303363432799));
#105622=CARTESIAN_POINT('Ctrl Pts',(110.932233234354,21.7396862567291,33.0378396653247));
#105623=CARTESIAN_POINT('Ctrl Pts',(111.018681842333,21.7185559447898,33.3453429873695));
#105624=CARTESIAN_POINT('Ctrl Pts',(110.93804168286,21.6974256328506,33.6999149686599));
#105625=CARTESIAN_POINT('Ctrl Pts',(110.727018157058,21.6762953209113,33.9397490113778));
#105626=CARTESIAN_POINT('Ctrl Pts',(110.515994631257,21.6551650089721,34.1795830540957));
#105627=CARTESIAN_POINT('Ctrl Pts',(110.174587739126,21.6340346970328,34.3046791582411));
#105628=CARTESIAN_POINT('Ctrl Pts',(109.858555314241,21.6129043850936,34.2580160922735));
#105629=CARTESIAN_POINT('Ctrl Pts',(109.542522889355,21.5917740731543,34.211353026306));
#105630=CARTESIAN_POINT('Ctrl Pts',(109.251864931714,21.5706437612151,33.9929307902253));
#105631=CARTESIAN_POINT('Ctrl Pts',(109.119139823187,21.5495134492758,33.702358702714));
#105632=CARTESIAN_POINT('Ctrl Pts',(109.062027344887,21.5404209384805,33.5773236417016));
#105633=CARTESIAN_POINT('Ctrl Pts',(109.034158296165,21.5313284276851,33.4389290477532));
#105634=CARTESIAN_POINT('Ctrl Pts',(109.034617182386,21.5222359168897,33.300357734449));
#105635=CARTESIAN_POINT('Origin',(110.,21.33,33.3));
#105636=CARTESIAN_POINT('',(109.03353070876,21.0642640831103,33.2991467029023));
#105637=CARTESIAN_POINT('',(109.033423686584,21.1222359168897,33.299130763016));
#105638=CARTESIAN_POINT('',(109.03325,21.33,33.3));
#105639=CARTESIAN_POINT('Ctrl Pts',(109.03353070876,21.0642640831103,33.2991467029023));
#105640=CARTESIAN_POINT('Ctrl Pts',(109.035565999728,21.079671572315,33.5332918739583));
#105641=CARTESIAN_POINT('Ctrl Pts',(109.121178897119,21.0950790615196,33.7687652483135));
#105642=CARTESIAN_POINT('Ctrl Pts',(109.275829590741,21.1104865507242,33.9429499406045));
#105643=CARTESIAN_POINT('Ctrl Pts',(109.487922382399,21.1316168626634,34.1818322681708));
#105644=CARTESIAN_POINT('Ctrl Pts',(109.829863092622,21.1527471746027,34.3054413942131));
#105645=CARTESIAN_POINT('Ctrl Pts',(110.145681380272,21.1738774865419,34.2573863849353));
#105646=CARTESIAN_POINT('Ctrl Pts',(110.461499667922,21.1950077984812,34.2093313756574));
#105647=CARTESIAN_POINT('Ctrl Pts',(110.751195532998,21.2161381104204,33.9896122310594));
#105648=CARTESIAN_POINT('Ctrl Pts',(110.882634883733,21.2372684223596,33.6984520452764));
#105649=CARTESIAN_POINT('Ctrl Pts',(111.014074234468,21.2583987342989,33.4072918594934));
#105650=CARTESIAN_POINT('Ctrl Pts',(110.987257070861,21.2795290462381,33.0446906325254));
#105651=CARTESIAN_POINT('Ctrl Pts',(110.814414356613,21.3006593581774,32.7760358858918));
#105652=CARTESIAN_POINT('Ctrl Pts',(110.641571642365,21.3217896701166,32.5073811392581));
#105653=CARTESIAN_POINT('Ctrl Pts',(110.322703377475,21.3429199820559,32.3326728729586));
#105654=CARTESIAN_POINT('Ctrl Pts',(110.003252067877,21.3640502939951,32.3315998746245));
#105655=CARTESIAN_POINT('Ctrl Pts',(109.683800758279,21.3851806059344,32.3305268762904));
#105656=CARTESIAN_POINT('Ctrl Pts',(109.363766403974,21.4063109178736,32.5030891459216));
#105657=CARTESIAN_POINT('Ctrl Pts',(109.189123176412,21.4274412298128,32.7705775262224));
#105658=CARTESIAN_POINT('Ctrl Pts',(109.087675518873,21.4397155142453,32.92595755429));
#105659=CARTESIAN_POINT('Ctrl Pts',(109.035286834209,21.4519897986778,33.1133682680862));
#105660=CARTESIAN_POINT('Ctrl Pts',(109.034572229009,21.4642640831103,33.3004087423462));
#105661=CARTESIAN_POINT('Ctrl Pts',(109.034617182386,21.5222359168897,33.300357734449));
#105662=CARTESIAN_POINT('Ctrl Pts',(109.035224713264,21.5101981157458,33.1168997269377));
#105663=CARTESIAN_POINT('Ctrl Pts',(109.085484798468,21.498160314602,32.9331319697948));
#105664=CARTESIAN_POINT('Ctrl Pts',(109.183272991379,21.4861225134581,32.7796457768268));
#105665=CARTESIAN_POINT('Ctrl Pts',(109.354923527512,21.4649922015189,32.510226877393));
#105666=CARTESIAN_POINT('Ctrl Pts',(109.67301685919,21.4438618895796,32.3341110174673));
#105667=CARTESIAN_POINT('Ctrl Pts',(109.992460670067,21.4227315776404,32.3316244033515));
#105668=CARTESIAN_POINT('Ctrl Pts',(110.311904480944,21.4016012657011,32.3291377892357));
#105669=CARTESIAN_POINT('Ctrl Pts',(110.632698771019,21.3804709537619,32.5002804209298));
#105670=CARTESIAN_POINT('Ctrl Pts',(110.808524459441,21.3593406418227,32.7669923979043));
#105671=CARTESIAN_POINT('Ctrl Pts',(110.984350147864,21.3382103298834,33.0337043748788));
#105672=CARTESIAN_POINT('Ctrl Pts',(111.015207234633,21.3170800179441,33.3959856971337));
#105673=CARTESIAN_POINT('Ctrl Pts',(110.887020531404,21.2959497060049,33.6885919760826));
#105674=CARTESIAN_POINT('Ctrl Pts',(110.758833828174,21.2748193940657,33.9811982550316));
#105675=CARTESIAN_POINT('Ctrl Pts',(110.471603334946,21.2536890821264,34.2041294906745));
#105676=CARTESIAN_POINT('Ctrl Pts',(110.15634071544,21.2325587701872,34.2557022170651));
#105677=CARTESIAN_POINT('Ctrl Pts',(109.841078095934,21.2114284582479,34.3072749434557));
#105678=CARTESIAN_POINT('Ctrl Pts',(109.49778335015,21.1902981463087,34.1874891605939));
#105679=CARTESIAN_POINT('Ctrl Pts',(109.283040527393,21.1691678343694,33.9509823500262));
#105680=CARTESIAN_POINT('Ctrl Pts',(109.124054194299,21.1535238618762,33.7758828981285));
#105681=CARTESIAN_POINT('Ctrl Pts',(109.035530815549,21.1378798893829,33.5368053411001));
#105682=CARTESIAN_POINT('Ctrl Pts',(109.033423686584,21.1222359168897,33.299130763016));
#105683=CARTESIAN_POINT('Origin',(110.,21.33,33.3));
#105684=CARTESIAN_POINT('',(109.03325,20.66675,33.3));
#105685=CARTESIAN_POINT('',(109.031713168497,20.7222359168897,33.3003348740849));
#105686=CARTESIAN_POINT('',(109.03325,21.33,33.3));
#105687=CARTESIAN_POINT('',(109.033986956687,20.66675,33.3377407293226));
#105688=CARTESIAN_POINT('Origin',(110.,20.66675,33.3));
#105689=CARTESIAN_POINT('Ctrl Pts',(109.033986956687,20.66675,33.3377407293226));
#105690=CARTESIAN_POINT('Ctrl Pts',(109.046513639301,20.6878803119393,33.6583741407962));
#105691=CARTESIAN_POINT('Ctrl Pts',(109.231527122784,20.7090106238785,33.9695692430953));
#105692=CARTESIAN_POINT('Ctrl Pts',(109.505777853249,20.7301409358178,34.1323692963055));
#105693=CARTESIAN_POINT('Ctrl Pts',(109.780028583713,20.751271247757,34.2951693495157));
#105694=CARTESIAN_POINT('Ctrl Pts',(110.143516561158,20.7724015596962,34.3095743536369));
#105695=CARTESIAN_POINT('Ctrl Pts',(110.429820581278,20.7935318716355,34.1679742283488));
#105696=CARTESIAN_POINT('Ctrl Pts',(110.716124601398,20.8146621835747,34.0263741030606));
#105697=CARTESIAN_POINT('Ctrl Pts',(110.925244664191,20.835792495514,33.728768848363));
#105698=CARTESIAN_POINT('Ctrl Pts',(110.961965060678,20.8569228074532,33.4113700988134));
#105699=CARTESIAN_POINT('Ctrl Pts',(110.998685457165,20.8780531193925,33.0939713492637));
#105700=CARTESIAN_POINT('Ctrl Pts',(110.863006187345,20.8991834313317,32.7567791048619));
#105701=CARTESIAN_POINT('Ctrl Pts',(110.616716338203,20.920313743271,32.553375562571));
#105702=CARTESIAN_POINT('Ctrl Pts',(110.37042648906,20.9414440552102,32.3499720202801));
#105703=CARTESIAN_POINT('Ctrl Pts',(110.013526060595,20.9625743671494,32.2803571801001));
#105704=CARTESIAN_POINT('Ctrl Pts',(109.708846083157,20.9837046790887,32.3763854624997));
#105705=CARTESIAN_POINT('Ctrl Pts',(109.404166105719,21.0048349910279,32.4724137448993));
#105706=CARTESIAN_POINT('Ctrl Pts',(109.151706579308,21.0259653029672,32.7340851498784));
#105707=CARTESIAN_POINT('Ctrl Pts',(109.066599252649,21.0470956149064,33.0419986169131));
#105708=CARTESIAN_POINT('Ctrl Pts',(109.043549231178,21.0528184376411,33.1253922835335));
#105709=CARTESIAN_POINT('Ctrl Pts',(109.032774738123,21.0585412603757,33.2121778729827));
#105710=CARTESIAN_POINT('Ctrl Pts',(109.03353070876,21.0642640831103,33.2991467029023));
#105711=CARTESIAN_POINT('Ctrl Pts',(109.033423686584,21.1222359168897,33.299130763016));
#105712=CARTESIAN_POINT('Ctrl Pts',(109.032684716686,21.1167495774437,33.2157783144218));
#105713=CARTESIAN_POINT('Ctrl Pts',(109.042574117077,21.1112632379977,33.132598418788));
#105714=CARTESIAN_POINT('Ctrl Pts',(109.063779996857,21.1057768985517,33.0524111404063));
#105715=CARTESIAN_POINT('Ctrl Pts',(109.14545318881,21.0846465866125,32.7435745796278));
#105716=CARTESIAN_POINT('Ctrl Pts',(109.394990472447,21.0635162746732,32.4791292963446));
#105717=CARTESIAN_POINT('Ctrl Pts',(109.698575654323,21.042385962734,32.379698479835));
#105718=CARTESIAN_POINT('Ctrl Pts',(110.0021608362,21.0212556507947,32.2802676633254));
#105719=CARTESIAN_POINT('Ctrl Pts',(110.359793916316,21.0001253388555,32.3458513135895));
#105720=CARTESIAN_POINT('Ctrl Pts',(110.608345300104,20.9789950269162,32.5465259310458));
#105721=CARTESIAN_POINT('Ctrl Pts',(110.856896683892,20.957864714977,32.7472005485021));
#105722=CARTESIAN_POINT('Ctrl Pts',(110.996366371352,20.9367344030377,33.0829661331506));
#105723=CARTESIAN_POINT('Ctrl Pts',(110.963152234546,20.9156040910985,33.4006936208202));
#105724=CARTESIAN_POINT('Ctrl Pts',(110.92993809774,20.8944737791592,33.7184211084898));
#105725=CARTESIAN_POINT('Ctrl Pts',(110.724040136667,20.87334346722,34.0181104991805));
#105726=CARTESIAN_POINT('Ctrl Pts',(110.439344866371,20.8522131552808,34.1630239200884));
#105727=CARTESIAN_POINT('Ctrl Pts',(110.154649596075,20.8310828433415,34.3079373409964));
#105728=CARTESIAN_POINT('Ctrl Pts',(109.791157016555,20.8099525314023,34.2980747921216));
#105729=CARTESIAN_POINT('Ctrl Pts',(109.51472120639,20.788822219463,34.1380282434287));
#105730=CARTESIAN_POINT('Ctrl Pts',(109.238285396225,20.7676919075238,33.9779816947357));
#105731=CARTESIAN_POINT('Ctrl Pts',(109.048906355415,20.7465615955845,33.6677511462246));
#105732=CARTESIAN_POINT('Ctrl Pts',(109.032832060182,20.7254312836453,33.3486399636312));
#105733=CARTESIAN_POINT('Ctrl Pts',(109.032021798148,20.7243661613934,33.3325544263057));
#105734=CARTESIAN_POINT('Ctrl Pts',(109.03165188566,20.7233010391415,33.3164463242016));
#105735=CARTESIAN_POINT('Ctrl Pts',(109.031713168497,20.7222359168897,33.3003348740849));
#105736=CARTESIAN_POINT('Origin',(110.,22.7327725593024,33.3));
#105737=CARTESIAN_POINT('',(109.261214578509,20.9327725593024,33.2993477253114));
#105738=CARTESIAN_POINT('',(109.259825220088,20.8537274406976,33.3002559833966));
#105739=CARTESIAN_POINT('',(109.261,22.7327725593024,33.3));
#105740=CARTESIAN_POINT('',(110.376335103234,20.66675,33.9374365499136));
#105741=CARTESIAN_POINT('Ctrl Pts',(109.261214578509,20.9327725593024,33.2993477253114));
#105742=CARTESIAN_POINT('Ctrl Pts',(109.260636701808,20.9270497365678,33.2328672853729));
#105743=CARTESIAN_POINT('Ctrl Pts',(109.299283346943,20.9001966018939,32.9215791476215));
#105744=CARTESIAN_POINT('Ctrl Pts',(109.737518843697,20.8522131552808,32.4673530790804));
#105745=CARTESIAN_POINT('Ctrl Pts',(110.555980958936,20.788822219463,32.6269973518284));
#105746=CARTESIAN_POINT('Ctrl Pts',(110.859421941756,20.7270011677028,33.3811136304354));
#105747=CARTESIAN_POINT('Ctrl Pts',(110.570443245433,20.6863104278818,33.8213655281161));
#105748=CARTESIAN_POINT('Ctrl Pts',(110.376335103234,20.66675,33.9374365499136));
#105749=CARTESIAN_POINT('',(110.723592507189,20.66675,33.1498837665692));
#105750=CARTESIAN_POINT('Origin',(110.,20.66675,33.3));
#105751=CARTESIAN_POINT('Ctrl Pts',(109.259825220088,20.8537274406976,33.3002559833966));
#105752=CARTESIAN_POINT('Ctrl Pts',(109.260707716465,20.8336622510103,33.0682449168145));
#105753=CARTESIAN_POINT('Ctrl Pts',(109.502678324612,20.7924667493836,32.590042208654));
#105754=CARTESIAN_POINT('Ctrl Pts',(110.316393411479,20.7301409358178,32.4870507258606));
#105755=CARTESIAN_POINT('Ctrl Pts',(110.6737668031,20.6878803119393,32.9097131646266));
#105756=CARTESIAN_POINT('Ctrl Pts',(110.723592507189,20.66675,33.1498837665692));
#105757=CARTESIAN_POINT('Origin',(110.,22.7327725593024,33.3));
#105758=CARTESIAN_POINT('',(109.262010734148,21.3327725593024,33.3003124495411));
#105759=CARTESIAN_POINT('',(109.261132768953,21.2537274406976,33.2993355405936));
#105760=CARTESIAN_POINT('',(109.261,22.7327725593024,33.3));
#105761=CARTESIAN_POINT('Ctrl Pts',(109.262010734148,21.3327725593024,33.3003124495411));
#105762=CARTESIAN_POINT('Ctrl Pts',(109.262556990412,21.3204982748699,33.1573355573992));
#105763=CARTESIAN_POINT('Ctrl Pts',(109.371544768259,21.2870936784982,32.7674521813911));
#105764=CARTESIAN_POINT('Ctrl Pts',(110.002931624722,21.2325587701872,32.4270088899107));
#105765=CARTESIAN_POINT('Ctrl Pts',(110.734176458714,21.1691678343694,32.8276587232552));
#105766=CARTESIAN_POINT('Ctrl Pts',(110.795674934758,21.1057768985517,33.6591941979777));
#105767=CARTESIAN_POINT('Ctrl Pts',(110.131329723613,21.042385962734,34.1630652541699));
#105768=CARTESIAN_POINT('Ctrl Pts',(109.417966198001,20.9847178496509,33.9051894315055));
#105769=CARTESIAN_POINT('Ctrl Pts',(109.262770389241,20.948180048507,33.4783322418983));
#105770=CARTESIAN_POINT('Ctrl Pts',(109.261214578509,20.9327725593024,33.2993477253114));
#105771=CARTESIAN_POINT('Ctrl Pts',(109.261132768953,21.2537274406976,33.2993355405936));
#105772=CARTESIAN_POINT('Ctrl Pts',(109.260567887903,21.2482411012516,33.2356195235146));
#105773=CARTESIAN_POINT('Ctrl Pts',(109.297242958642,21.2216244498664,32.9271449511855));
#105774=CARTESIAN_POINT('Ctrl Pts',(109.728271023269,21.1738774865419,32.4703661604886));
#105775=CARTESIAN_POINT('Ctrl Pts',(110.548413292333,21.1104865507242,32.6207659046162));
#105776=CARTESIAN_POINT('Ctrl Pts',(110.868252234251,21.0470956149064,33.3907605269755));
#105777=CARTESIAN_POINT('Ctrl Pts',(110.39607661522,20.9837046790887,34.0780233965501));
#105778=CARTESIAN_POINT('Ctrl Pts',(109.56249704574,20.9203137432709,34.0554061006045));
#105779=CARTESIAN_POINT('Ctrl Pts',(109.265670790959,20.8769879971406,33.5691613111105));
#105780=CARTESIAN_POINT('Ctrl Pts',(109.259778374454,20.8547925629495,33.3125718475149));
#105781=CARTESIAN_POINT('Ctrl Pts',(109.259825220088,20.8537274406976,33.3002559833966));
#105782=CARTESIAN_POINT('Origin',(110.,22.7327725593024,33.3));
#105783=CARTESIAN_POINT('',(109.260096259818,21.7327725593024,33.3004698838673));
#105784=CARTESIAN_POINT('',(109.262045097267,21.6537274406976,33.3002734582445));
#105785=CARTESIAN_POINT('',(109.261,22.7327725593024,33.3));
#105786=CARTESIAN_POINT('Ctrl Pts',(109.260096259818,21.7327725593024,33.3004698838673));
#105787=CARTESIAN_POINT('Ctrl Pts',(109.261654463222,21.713946813172,33.0826444252441));
#105788=CARTESIAN_POINT('Ctrl Pts',(109.478357859312,21.6739907551024,32.6175592866656));
#105789=CARTESIAN_POINT('Ctrl Pts',(110.268062035357,21.6129043850936,32.4691917393687));
#105790=CARTESIAN_POINT('Ctrl Pts',(110.842979873719,21.5495134492758,33.0730612101061));
#105791=CARTESIAN_POINT('Ctrl Pts',(110.648917258071,21.4861225134581,33.8839824667209));
#105792=CARTESIAN_POINT('Ctrl Pts',(109.86287719836,21.4227315776404,34.1621579965021));
#105793=CARTESIAN_POINT('Ctrl Pts',(109.329908345882,21.3716149262551,33.7522685476019));
#105794=CARTESIAN_POINT('Ctrl Pts',(109.261616604411,21.3416285868091,33.4034718065368));
#105795=CARTESIAN_POINT('Ctrl Pts',(109.262010734148,21.3327725593024,33.3003124495411));
#105796=CARTESIAN_POINT('Ctrl Pts',(109.262045097267,21.6537274406976,33.3002734582445));
#105797=CARTESIAN_POINT('Ctrl Pts',(109.262509504114,21.6416896395538,33.1600350640879));
#105798=CARTESIAN_POINT('Ctrl Pts',(109.36836833146,21.6085215264707,32.7729796264293));
#105799=CARTESIAN_POINT('Ctrl Pts',(109.993204480012,21.5542231014483,32.4270322435203));
#105800=CARTESIAN_POINT('Ctrl Pts',(110.72886617238,21.4908321656306,32.8195051832315));
#105801=CARTESIAN_POINT('Ctrl Pts',(110.799629204568,21.4274412298128,33.6503070362846));
#105802=CARTESIAN_POINT('Ctrl Pts',(110.140937708849,21.3640502939951,34.1615442221346));
#105803=CARTESIAN_POINT('Ctrl Pts',(109.421812448308,21.3061456976234,33.9106199555457));
#105804=CARTESIAN_POINT('Ctrl Pts',(109.262743493862,21.2693714131909,33.4810179954207));
#105805=CARTESIAN_POINT('Ctrl Pts',(109.261132768953,21.2537274406976,33.2993355405936));
#105806=CARTESIAN_POINT('Origin',(110.,20.66675,33.3));
#105807=CARTESIAN_POINT('Ctrl Pts',(110.376335103234,20.66675,33.9374365499136));
#105808=CARTESIAN_POINT('Ctrl Pts',(110.362051118216,20.66675,33.9491714998516));
#105809=CARTESIAN_POINT('Ctrl Pts',(110.347327113967,20.66675,33.9603101779496));
#105810=CARTESIAN_POINT('Ctrl Pts',(110.33218889002,20.66675,33.9708180297552));
#105811=CARTESIAN_POINT('Ctrl Pts',(110.304729416617,20.66675,33.9898783949733));
#105812=CARTESIAN_POINT('Ctrl Pts',(110.275909391602,20.66675,34.0068653774463));
#105813=CARTESIAN_POINT('Ctrl Pts',(110.245983179273,20.66675,34.0218215741852));
#105814=CARTESIAN_POINT('Ctrl Pts',(110.233763985821,20.66675,34.0279283497184));
#105815=CARTESIAN_POINT('Ctrl Pts',(110.221359914847,20.66675,34.0336962029393));
#105816=CARTESIAN_POINT('Ctrl Pts',(110.208786594842,20.66675,34.0391264878303));
#105817=CARTESIAN_POINT('Ctrl Pts',(110.201157085926,20.66675,34.042421592622));
#105818=CARTESIAN_POINT('Ctrl Pts',(110.19346825675,20.66675,34.0455909818006));
#105819=CARTESIAN_POINT('Ctrl Pts',(110.185731523892,20.66675,34.0486322638215));
#105820=CARTESIAN_POINT('Ctrl Pts',(110.152517375499,20.66675,34.0616886267858));
#105821=CARTESIAN_POINT('Ctrl Pts',(110.118382926888,20.66675,34.0724046024287));
#105822=CARTESIAN_POINT('Ctrl Pts',(110.083616565184,20.66675,34.080825390986));
#105823=CARTESIAN_POINT('Ctrl Pts',(110.058360083766,20.66675,34.0869427837557));
#105824=CARTESIAN_POINT('Ctrl Pts',(110.03276907629,20.66675,34.0918481845548));
#105825=CARTESIAN_POINT('Ctrl Pts',(110.006943547618,20.66675,34.0955457613206));
#105826=CARTESIAN_POINT('Ctrl Pts',(109.999025934563,20.66675,34.0966793676233));
#105827=CARTESIAN_POINT('Ctrl Pts',(109.991089910533,20.66675,34.0976987562079));
#105828=CARTESIAN_POINT('Ctrl Pts',(109.983146762188,20.66675,34.0986034204503));
#105829=CARTESIAN_POINT('Ctrl Pts',(109.945618729961,20.66675,34.1028775781728));
#105830=CARTESIAN_POINT('Ctrl Pts',(109.907880244829,20.66675,34.1046023075043));
#105831=CARTESIAN_POINT('Ctrl Pts',(109.870239318907,20.66675,34.1038241003379));
#105832=CARTESIAN_POINT('Ctrl Pts',(109.83232030645,20.66675,34.1030401438725));
#105833=CARTESIAN_POINT('Ctrl Pts',(109.794498983599,20.66675,34.0997165237621));
#105834=CARTESIAN_POINT('Ctrl Pts',(109.757066157873,20.66675,34.0938532556067));
#105835=CARTESIAN_POINT('Ctrl Pts',(109.737844223589,20.66675,34.0908424394849));
#105836=CARTESIAN_POINT('Ctrl Pts',(109.718724464461,20.66675,34.0871611482163));
#105837=CARTESIAN_POINT('Ctrl Pts',(109.69974559798,20.66675,34.0828040554303));
#105838=CARTESIAN_POINT('Ctrl Pts',(109.690444770713,20.66675,34.0806688084476));
#105839=CARTESIAN_POINT('Ctrl Pts',(109.681175436593,20.66675,34.0783703804502));
#105840=CARTESIAN_POINT('Ctrl Pts',(109.671964996317,20.66675,34.0759144833926));
#105841=CARTESIAN_POINT('Ctrl Pts',(109.634271818598,20.66675,34.0658638711018));
#105842=CARTESIAN_POINT('Ctrl Pts',(109.597484896717,20.66675,34.0531628165186));
#105843=CARTESIAN_POINT('Ctrl Pts',(109.561907952814,20.66675,34.0378349421013));
#105844=CARTESIAN_POINT('Ctrl Pts',(109.527210364415,20.66675,34.0228859268347));
#105845=CARTESIAN_POINT('Ctrl Pts',(109.493662072607,20.66675,34.0054388458726));
#105846=CARTESIAN_POINT('Ctrl Pts',(109.461373044813,20.66675,33.985736470523));
#105847=CARTESIAN_POINT('Ctrl Pts',(109.446367008596,20.66675,33.9765799681977));
#105848=CARTESIAN_POINT('Ctrl Pts',(109.431633085047,20.66675,33.9669356125781));
#105849=CARTESIAN_POINT('Ctrl Pts',(109.417183333681,20.66675,33.9568241627759));
#105850=CARTESIAN_POINT('Ctrl Pts',(109.409788076771,20.66675,33.9516492108251));
#105851=CARTESIAN_POINT('Ctrl Pts',(109.402467266531,20.66675,33.946351878214));
#105852=CARTESIAN_POINT('Ctrl Pts',(109.39522261568,20.66675,33.9409347405269));
#105853=CARTESIAN_POINT('Ctrl Pts',(109.389483833801,20.66675,33.9366436059738));
#105854=CARTESIAN_POINT('Ctrl Pts',(109.383794686831,20.66675,33.9322785792095));
#105855=CARTESIAN_POINT('Ctrl Pts',(109.378162977365,20.66675,33.9278468206238));
#105856=CARTESIAN_POINT('Ctrl Pts',(109.347071246258,20.66675,33.9033798187109));
#105857=CARTESIAN_POINT('Ctrl Pts',(109.317666910692,20.66675,33.8768368840104));
#105858=CARTESIAN_POINT('Ctrl Pts',(109.290062958723,20.66675,33.848495844236));
#105859=CARTESIAN_POINT('Ctrl Pts',(109.261797091972,20.66675,33.8194752150602));
#105860=CARTESIAN_POINT('Ctrl Pts',(109.235418059424,20.66675,33.7885686279158));
#105861=CARTESIAN_POINT('Ctrl Pts',(109.211065944257,20.66675,33.7560230457913));
#105862=CARTESIAN_POINT('Ctrl Pts',(109.199623874339,20.66675,33.7407311985079));
#105863=CARTESIAN_POINT('Ctrl Pts',(109.188629635713,20.66675,33.7250768436632));
#105864=CARTESIAN_POINT('Ctrl Pts',(109.17810006173,20.66675,33.709082429934));
#105865=CARTESIAN_POINT('Ctrl Pts',(109.17231735898,20.66675,33.7002985094835));
#105866=CARTESIAN_POINT('Ctrl Pts',(109.166674831446,20.66675,33.6914119930594));
#105867=CARTESIAN_POINT('Ctrl Pts',(109.161175505246,20.66675,33.6824263847011));
#105868=CARTESIAN_POINT('Ctrl Pts',(109.156958433143,20.66675,33.6755359117666));
#105869=CARTESIAN_POINT('Ctrl Pts',(109.152828330105,20.66675,33.6685915480918));
#105870=CARTESIAN_POINT('Ctrl Pts',(109.148789996522,20.66675,33.661601815363));
#105871=CARTESIAN_POINT('Ctrl Pts',(109.127615458512,20.66675,33.6249519551497));
#105872=CARTESIAN_POINT('Ctrl Pts',(109.108928594472,20.66675,33.5870044942501));
#105873=CARTESIAN_POINT('Ctrl Pts',(109.092867816801,20.66675,33.548034950299));
#105874=CARTESIAN_POINT('Ctrl Pts',(109.076912664157,20.66675,33.5093216927643));
#105875=CARTESIAN_POINT('Ctrl Pts',(109.063548303014,20.66675,33.4695987840075));
#105876=CARTESIAN_POINT('Ctrl Pts',(109.052944594755,20.66675,33.4290994676753));
#105877=CARTESIAN_POINT('Ctrl Pts',(109.045075862302,20.66675,33.3990459923237));
#105878=CARTESIAN_POINT('Ctrl Pts',(109.038727971098,20.66675,33.368564132549));
#105879=CARTESIAN_POINT('Ctrl Pts',(109.033986956687,20.66675,33.3377407293226));
#105880=CARTESIAN_POINT('',(109.377034789147,20.66675,32.5586406032643));
#105881=CARTESIAN_POINT('Origin',(110.,20.66675,33.3));
#105882=CARTESIAN_POINT('Ctrl Pts',(109.377024795358,20.66675,32.5586208180317));
#105883=CARTESIAN_POINT('Ctrl Pts',(109.396809806408,20.66675,32.5453690358772));
#105884=CARTESIAN_POINT('Ctrl Pts',(109.417086018765,20.66675,32.5329219386122));
#105885=CARTESIAN_POINT('Ctrl Pts',(109.437834479318,20.66675,32.521328234985));
#105886=CARTESIAN_POINT('Ctrl Pts',(109.470704923652,20.66675,32.5029610800471));
#105887=CARTESIAN_POINT('Ctrl Pts',(109.504760685105,20.66675,32.4867341891181));
#105888=CARTESIAN_POINT('Ctrl Pts',(109.53977975488,20.66675,32.472656252588));
#105889=CARTESIAN_POINT('Ctrl Pts',(109.559613981063,20.66675,32.4646827404667));
#105890=CARTESIAN_POINT('Ctrl Pts',(109.57975732631,20.66675,32.4573991898274));
#105891=CARTESIAN_POINT('Ctrl Pts',(109.600169285294,20.66675,32.4508117735884));
#105892=CARTESIAN_POINT('Ctrl Pts',(109.609416808786,20.66675,32.4478273816213));
#105893=CARTESIAN_POINT('Ctrl Pts',(109.618717903772,20.66675,32.4449865447394));
#105894=CARTESIAN_POINT('Ctrl Pts',(109.628057331603,20.66675,32.4422928045765));
#105895=CARTESIAN_POINT('Ctrl Pts',(109.66815554816,20.66675,32.4307274090985));
#105896=CARTESIAN_POINT('Ctrl Pts',(109.709018022693,20.66675,32.4218504694604));
#105897=CARTESIAN_POINT('Ctrl Pts',(109.75033803836,20.66675,32.4156791778283));
#105898=CARTESIAN_POINT('Ctrl Pts',(109.774132683495,20.66675,32.4121253627575));
#105899=CARTESIAN_POINT('Ctrl Pts',(109.798079053289,20.66675,32.4094697570998));
#105900=CARTESIAN_POINT('Ctrl Pts',(109.822116736403,20.66675,32.4077233113639));
#105901=CARTESIAN_POINT('Ctrl Pts',(109.832278466539,20.66675,32.4069850159889));
#105902=CARTESIAN_POINT('Ctrl Pts',(109.842456487862,20.66675,32.4064092642038));
#105903=CARTESIAN_POINT('Ctrl Pts',(109.852646091747,20.66675,32.4059971752793));
#105904=CARTESIAN_POINT('Ctrl Pts',(109.861010040807,20.66675,32.4056589196601));
#105905=CARTESIAN_POINT('Ctrl Pts',(109.869372278937,20.66675,32.4054313258998));
#105906=CARTESIAN_POINT('Ctrl Pts',(109.877729756577,20.66675,32.4053143381012));
#105907=CARTESIAN_POINT('Ctrl Pts',(109.91781820896,20.66675,32.4047531807764));
#105908=CARTESIAN_POINT('Ctrl Pts',(109.957802808996,20.66675,32.406732837445));
#105909=CARTESIAN_POINT('Ctrl Pts',(109.997408074228,20.66675,32.41127414139));
#105910=CARTESIAN_POINT('Ctrl Pts',(110.03608830874,20.66675,32.4157093774766));
#105911=CARTESIAN_POINT('Ctrl Pts',(110.074407739332,20.66675,32.4225883582893));
#105912=CARTESIAN_POINT('Ctrl Pts',(110.112088050043,20.66675,32.4319736180715));
#105913=CARTESIAN_POINT('Ctrl Pts',(110.1299959605,20.66675,32.4364340481643));
#105914=CARTESIAN_POINT('Ctrl Pts',(110.147759098548,20.66675,32.4414611782776));
#105915=CARTESIAN_POINT('Ctrl Pts',(110.165344832615,20.66675,32.4470649103973));
#105916=CARTESIAN_POINT('Ctrl Pts',(110.173110216502,20.66675,32.4495393667345));
#105917=CARTESIAN_POINT('Ctrl Pts',(110.180840981897,20.66675,32.4521262789321));
#105918=CARTESIAN_POINT('Ctrl Pts',(110.188534182193,20.66675,32.4548266220958));
#105919=CARTESIAN_POINT('Ctrl Pts',(110.196113058415,20.66675,32.457486837066));
#105920=CARTESIAN_POINT('Ctrl Pts',(110.203647475052,20.66675,32.4602543667076));
#105921=CARTESIAN_POINT('Ctrl Pts',(110.211131498076,20.66675,32.4631281412987));
#105922=CARTESIAN_POINT('Ctrl Pts',(110.24432115308,20.66675,32.4758725685853));
#105923=CARTESIAN_POINT('Ctrl Pts',(110.276544706183,20.66675,32.4907119074751));
#105924=CARTESIAN_POINT('Ctrl Pts',(110.307588054684,20.66675,32.507684733064));
#105925=CARTESIAN_POINT('Ctrl Pts',(110.33659439538,20.66675,32.5235438328514));
#105926=CARTESIAN_POINT('Ctrl Pts',(110.364570383607,20.66675,32.5412666417595));
#105927=CARTESIAN_POINT('Ctrl Pts',(110.391403599684,20.66675,32.5607050382317));
#105928=CARTESIAN_POINT('Ctrl Pts',(110.405014168788,20.66675,32.5705647448612));
#105929=CARTESIAN_POINT('Ctrl Pts',(110.418330348652,20.66675,32.5808661044064));
#105930=CARTESIAN_POINT('Ctrl Pts',(110.43133494341,20.66675,32.5915910088429));
#105931=CARTESIAN_POINT('Ctrl Pts',(110.440046433796,20.66675,32.5987753851059));
#105932=CARTESIAN_POINT('Ctrl Pts',(110.448618068475,20.66675,32.6061498360859));
#105933=CARTESIAN_POINT('Ctrl Pts',(110.457044207542,20.66675,32.6137090329155));
#105934=CARTESIAN_POINT('Ctrl Pts',(110.46402254411,20.66675,32.6199693876567));
#105935=CARTESIAN_POINT('Ctrl Pts',(110.470902598729,20.66675,32.6263581673401));
#105936=CARTESIAN_POINT('Ctrl Pts',(110.477664901628,20.66675,32.6328561811291));
#105937=CARTESIAN_POINT('Ctrl Pts',(110.504570931299,20.66675,32.658710650293));
#105938=CARTESIAN_POINT('Ctrl Pts',(110.52967598653,20.66675,32.6863438203501));
#105939=CARTESIAN_POINT('Ctrl Pts',(110.55282817067,20.66675,32.715530046899));
#105940=CARTESIAN_POINT('Ctrl Pts',(110.575716238353,20.66675,32.7443833215888));
#105941=CARTESIAN_POINT('Ctrl Pts',(110.596696157522,20.66675,32.7747556685919));
#105942=CARTESIAN_POINT('Ctrl Pts',(110.6155730175,20.66675,32.8064437120442));
#105943=CARTESIAN_POINT('Ctrl Pts',(110.624095911369,20.66675,32.8207508495441));
#105944=CARTESIAN_POINT('Ctrl Pts',(110.632189398688,20.66675,32.83532628065));
#105945=CARTESIAN_POINT('Ctrl Pts',(110.639831931783,20.66675,32.85015126595));
#105946=CARTESIAN_POINT('Ctrl Pts',(110.643387138242,20.66675,32.8570476552539));
#105947=CARTESIAN_POINT('Ctrl Pts',(110.646845565571,20.66675,32.8639998037261));
#105948=CARTESIAN_POINT('Ctrl Pts',(110.650202196263,20.66675,32.8710002002437));
#105949=CARTESIAN_POINT('Ctrl Pts',(110.665521542891,20.66675,32.9029493512352));
#105950=CARTESIAN_POINT('Ctrl Pts',(110.67866190767,20.66675,32.9357692553209));
#105951=CARTESIAN_POINT('Ctrl Pts',(110.689468386051,20.66675,32.9692696922969));
#105952=CARTESIAN_POINT('Ctrl Pts',(110.699880421221,20.66675,33.0015473423944));
#105953=CARTESIAN_POINT('Ctrl Pts',(110.70812586013,20.66675,33.0344577142209));
#105954=CARTESIAN_POINT('Ctrl Pts',(110.714018973751,20.66675,33.0678288587027));
#105955=CARTESIAN_POINT('Ctrl Pts',(110.718801298005,20.66675,33.09490989666));
#105956=CARTESIAN_POINT('Ctrl Pts',(110.722033682588,20.66675,33.1222945339637));
#105957=CARTESIAN_POINT('Ctrl Pts',(110.723592507189,20.66675,33.1498837665692));
#105958=CARTESIAN_POINT('Ctrl Pts',(109.675031770393,22.1247415238079,33.9637142832168));
#105959=CARTESIAN_POINT('Ctrl Pts',(109.454735599089,22.1036112118687,33.8558527250311));
#105960=CARTESIAN_POINT('Ctrl Pts',(109.133967345731,22.0613505879902,33.4047795537825));
#105961=CARTESIAN_POINT('Ctrl Pts',(109.440802503731,21.9979596521725,32.6290335730239));
#105962=CARTESIAN_POINT('Ctrl Pts',(110.258915539699,21.9345687163547,32.4663782012585));
#105963=CARTESIAN_POINT('Ctrl Pts',(110.840340273426,21.871177780537,33.0636201432557));
#105964=CARTESIAN_POINT('Ctrl Pts',(110.655412180794,21.8077868447193,33.8767425456563));
#105965=CARTESIAN_POINT('Ctrl Pts',(109.87248062677,21.7443959089015,34.1636192592745));
#105966=CARTESIAN_POINT('Ctrl Pts',(109.205929096291,21.6810049730838,33.6627223392945));
#105967=CARTESIAN_POINT('Ctrl Pts',(109.263736762059,21.6176140372661,32.8309100417672));
#105968=CARTESIAN_POINT('Ctrl Pts',(109.993204480012,21.5542231014483,32.4270322435203));
#105969=CARTESIAN_POINT('Ctrl Pts',(110.72886617238,21.4908321656306,32.8195051832315));
#105970=CARTESIAN_POINT('Ctrl Pts',(110.799629204568,21.4274412298128,33.6503070362846));
#105971=CARTESIAN_POINT('Ctrl Pts',(110.140937708849,21.3640502939951,34.1615442221346));
#105972=CARTESIAN_POINT('Ctrl Pts',(109.353676833335,21.3006593581774,33.8868454058899));
#105973=CARTESIAN_POINT('Ctrl Pts',(109.156019502377,21.2372684223596,33.0768054602444));
#105974=CARTESIAN_POINT('Ctrl Pts',(109.728271023269,21.1738774865419,32.4703661604886));
#105975=CARTESIAN_POINT('Ctrl Pts',(110.548413292333,21.1104865507242,32.6207659046162));
#105976=CARTESIAN_POINT('Ctrl Pts',(110.868252234251,21.0470956149064,33.3907605269755));
#105977=CARTESIAN_POINT('Ctrl Pts',(110.39607661522,20.9837046790887,34.0780233965501));
#105978=CARTESIAN_POINT('Ctrl Pts',(109.56249704574,20.9203137432709,34.0554061006045));
#105979=CARTESIAN_POINT('Ctrl Pts',(109.128203450212,20.8569228074532,33.3439697147248));
#105980=CARTESIAN_POINT('Ctrl Pts',(109.488772271949,20.7935318716355,32.5918022902927));
#105981=CARTESIAN_POINT('Ctrl Pts',(110.316393411479,20.7301409358178,32.4870507258606));
#105982=CARTESIAN_POINT('Ctrl Pts',(110.6737668031,20.6878803119393,32.9097131646266));
#105983=CARTESIAN_POINT('Ctrl Pts',(110.723592507189,20.66675,33.1498837665692));
#105984=CARTESIAN_POINT('Ctrl Pts',(109.641648137424,22.080911015872,34.0318969300381));
#105985=CARTESIAN_POINT('Ctrl Pts',(109.398721179915,22.0597807039327,33.9129548712313));
#105986=CARTESIAN_POINT('Ctrl Pts',(109.045000752583,22.0175200800542,33.4155434434415));
#105987=CARTESIAN_POINT('Ctrl Pts',(109.383356752817,21.9541291442365,32.5601059213578));
#105988=CARTESIAN_POINT('Ctrl Pts',(110.285513651637,21.8907382084188,32.3807411400661));
#105989=CARTESIAN_POINT('Ctrl Pts',(110.926667516219,21.827347272601,33.0393370975301));
#105990=CARTESIAN_POINT('Ctrl Pts',(110.722741961658,21.7639563367833,33.935990680421));
#105991=CARTESIAN_POINT('Ctrl Pts',(109.859380700179,21.7005654009655,34.2523379269785));
#105992=CARTESIAN_POINT('Ctrl Pts',(109.124355055552,21.6371744651478,33.6999844109113));
#105993=CARTESIAN_POINT('Ctrl Pts',(109.188101239984,21.5737835293301,32.7827209402844));
#105994=CARTESIAN_POINT('Ctrl Pts',(109.992506383631,21.5103925935123,32.3373532148607));
#105995=CARTESIAN_POINT('Ctrl Pts',(110.803741801951,21.4470016576946,32.7701444730289));
#105996=CARTESIAN_POINT('Ctrl Pts',(110.881774243513,21.3836107218769,33.6862936973193));
#105997=CARTESIAN_POINT('Ctrl Pts',(110.155416086472,21.3202197860591,34.2500497235289));
#105998=CARTESIAN_POINT('Ctrl Pts',(109.287280757012,21.2568288502414,33.9471313965039));
#105999=CARTESIAN_POINT('Ctrl Pts',(109.069318303309,21.1934379144237,33.0538769278));
#106000=CARTESIAN_POINT('Ctrl Pts',(109.700356600874,21.1300469786059,32.3851387780128));
#106001=CARTESIAN_POINT('Ctrl Pts',(110.6047511937,21.0666560427882,32.550988924362));
#106002=CARTESIAN_POINT('Ctrl Pts',(110.957446842438,21.0032651069704,33.40008425725));
#106003=CARTESIAN_POINT('Ctrl Pts',(110.436765135345,20.9398741711527,34.1579488943238));
#106004=CARTESIAN_POINT('Ctrl Pts',(109.517552842839,20.876483235335,34.133008148152));
#106005=CARTESIAN_POINT('Ctrl Pts',(109.038644738343,20.8130922995172,33.3484866757211));
#106006=CARTESIAN_POINT('Ctrl Pts',(109.436254403179,20.7497013636995,32.519049909424));
#106007=CARTESIAN_POINT('Ctrl Pts',(110.348896162703,20.6863104278818,32.4035373306486));
#106008=CARTESIAN_POINT('Ctrl Pts',(110.742982134361,20.6440498040033,32.8696194222918));
#106009=CARTESIAN_POINT('Ctrl Pts',(110.797926378868,20.622919492064,33.1344624890934));
#106010=CARTESIAN_POINT('Ctrl Pts',(109.608264504454,22.037080507936,34.1000795768593));
#106011=CARTESIAN_POINT('Ctrl Pts',(109.342706760742,22.0159501959967,33.9700570174315));
#106012=CARTESIAN_POINT('Ctrl Pts',(108.956034159435,21.9736895721183,33.4263073331004));
#106013=CARTESIAN_POINT('Ctrl Pts',(109.325911001904,21.9102986363005,32.4911782696917));
#106014=CARTESIAN_POINT('Ctrl Pts',(110.312111763575,21.8469077004828,32.2951040788738));
#106015=CARTESIAN_POINT('Ctrl Pts',(111.012994759013,21.783516764665,33.0150540518046));
#106016=CARTESIAN_POINT('Ctrl Pts',(110.790071742523,21.7201258288473,33.9952388151856));
#106017=CARTESIAN_POINT('Ctrl Pts',(109.846280773588,21.6567348930296,34.3410565946825));
#106018=CARTESIAN_POINT('Ctrl Pts',(109.042781014812,21.5933439572118,33.737246482528));
#106019=CARTESIAN_POINT('Ctrl Pts',(109.112465717909,21.5299530213941,32.7345318388015));
#106020=CARTESIAN_POINT('Ctrl Pts',(109.99180828725,21.4665620855764,32.2476741862011));
#106021=CARTESIAN_POINT('Ctrl Pts',(110.878617431523,21.4031711497586,32.7207837628264));
#106022=CARTESIAN_POINT('Ctrl Pts',(110.963919282458,21.3397802139409,33.7222803583539));
#106023=CARTESIAN_POINT('Ctrl Pts',(110.169894464095,21.2763892781232,34.3385552249232));
#106024=CARTESIAN_POINT('Ctrl Pts',(109.220884680689,21.2129983423054,34.007417387118));
#106025=CARTESIAN_POINT('Ctrl Pts',(108.982617104241,21.1496074064877,33.0309483953555));
#106026=CARTESIAN_POINT('Ctrl Pts',(109.672442178479,21.0862164706699,32.2999113955371));
#106027=CARTESIAN_POINT('Ctrl Pts',(110.661089095066,21.0228255348522,32.4812119441078));
#106028=CARTESIAN_POINT('Ctrl Pts',(111.046641450625,20.9594345990345,33.4094079875246));
#106029=CARTESIAN_POINT('Ctrl Pts',(110.47745365547,20.8960436632168,34.2378743920975));
#106030=CARTESIAN_POINT('Ctrl Pts',(109.472608639937,20.832652727399,34.2106101956994));
#106031=CARTESIAN_POINT('Ctrl Pts',(108.949086026474,20.7692617915813,33.3530036367172));
#106032=CARTESIAN_POINT('Ctrl Pts',(109.383736534408,20.7058708557635,32.4462975285553));
#106033=CARTESIAN_POINT('Ctrl Pts',(110.381398913927,20.6424799199458,32.3200239354364));
#106034=CARTESIAN_POINT('Ctrl Pts',(110.812197465622,20.6002192960673,32.8295256799569));
#106035=CARTESIAN_POINT('Ctrl Pts',(110.872260250547,20.5790889841281,33.1190412116176));
#106036=CARTESIAN_POINT('Ctrl Pts',(109.574880871485,21.99325,34.1682622236805));
#106037=CARTESIAN_POINT('Ctrl Pts',(109.286692341569,21.9721196880608,34.0271591636317));
#106038=CARTESIAN_POINT('Ctrl Pts',(108.867067566286,21.9298590641823,33.4370712227594));
#106039=CARTESIAN_POINT('Ctrl Pts',(109.26846525099,21.8664681283645,32.4222506180256));
#106040=CARTESIAN_POINT('Ctrl Pts',(110.338709875513,21.8030771925468,32.2094670176815));
#106041=CARTESIAN_POINT('Ctrl Pts',(111.099322001806,21.7396862567291,32.9907710060791));
#106042=CARTESIAN_POINT('Ctrl Pts',(110.857401523387,21.6762953209113,34.0544869499503));
#106043=CARTESIAN_POINT('Ctrl Pts',(109.833180846996,21.6129043850936,34.4297752623866));
#106044=CARTESIAN_POINT('Ctrl Pts',(108.961206974073,21.5495134492758,33.7745085541447));
#106045=CARTESIAN_POINT('Ctrl Pts',(109.036830195834,21.4861225134581,32.6863427373186));
#106046=CARTESIAN_POINT('Ctrl Pts',(109.991110190869,21.4227315776404,32.1579951575416));
#106047=CARTESIAN_POINT('Ctrl Pts',(110.953493061094,21.3593406418227,32.6714230526239));
#106048=CARTESIAN_POINT('Ctrl Pts',(111.046064321402,21.2959497060049,33.7582670193886));
#106049=CARTESIAN_POINT('Ctrl Pts',(110.184372841718,21.2325587701872,34.4270607263175));
#106050=CARTESIAN_POINT('Ctrl Pts',(109.154488604366,21.1691678343694,34.0677033777321));
#106051=CARTESIAN_POINT('Ctrl Pts',(108.895915905173,21.1057768985517,33.0080198629111));
#106052=CARTESIAN_POINT('Ctrl Pts',(109.644527756083,21.042385962734,32.2146840130614));
#106053=CARTESIAN_POINT('Ctrl Pts',(110.717426996432,20.9789950269162,32.4114349638535));
#106054=CARTESIAN_POINT('Ctrl Pts',(111.135836058812,20.9156040910985,33.4187317177991));
#106055=CARTESIAN_POINT('Ctrl Pts',(110.518142175595,20.8522131552808,34.3177998898711));
#106056=CARTESIAN_POINT('Ctrl Pts',(109.427664437036,20.788822219463,34.2882122432469));
#106057=CARTESIAN_POINT('Ctrl Pts',(108.859527314605,20.7254312836453,33.3575205977135));
#106058=CARTESIAN_POINT('Ctrl Pts',(109.331218665638,20.6620403478275,32.3735451476867));
#106059=CARTESIAN_POINT('Ctrl Pts',(110.413901665152,20.5986494120098,32.2365105402243));
#106060=CARTESIAN_POINT('Ctrl Pts',(110.881412796884,20.5563887881313,32.7894319376221));
#106061=CARTESIAN_POINT('Ctrl Pts',(110.946594122226,20.5352584761921,33.1036199341418));
#106062=CARTESIAN_POINT('Ctrl Pts',(109.031713168497,20.7222359168897,33.3003348740849));
#106063=CARTESIAN_POINT('Ctrl Pts',(109.032777313761,20.7037406112598,33.0205677454497));
#106064=CARTESIAN_POINT('Ctrl Pts',(109.163857863559,20.6852453056299,32.7397911054646));
#106065=CARTESIAN_POINT('Ctrl Pts',(109.377024795358,20.66675,32.5586208180318));
#106066=CARTESIAN_POINT('',(109.570122622048,21.99325,32.6988956497206));
#106067=CARTESIAN_POINT('Ctrl Pts',(109.569164649808,21.99325,32.6980580125958));
#106068=CARTESIAN_POINT('Ctrl Pts',(109.552656141457,21.99325,32.7063773006967));
#106069=CARTESIAN_POINT('Ctrl Pts',(109.536515068327,21.99325,32.7153401328564));
#106070=CARTESIAN_POINT('Ctrl Pts',(109.520783466014,21.99325,32.7249368845833));
#106071=CARTESIAN_POINT('Ctrl Pts',(109.492247653832,21.99325,32.7423445903831));
#106072=CARTESIAN_POINT('Ctrl Pts',(109.465058040893,21.99325,32.7618350277424));
#106073=CARTESIAN_POINT('Ctrl Pts',(109.439278518602,21.99325,32.7831583285348));
#106074=CARTESIAN_POINT('Ctrl Pts',(109.428752468441,21.99325,32.7918648565767));
#106075=CARTESIAN_POINT('Ctrl Pts',(109.418461644647,21.99325,32.8008775159162));
#106076=CARTESIAN_POINT('Ctrl Pts',(109.408411128155,21.99325,32.8101814651125));
#106077=CARTESIAN_POINT('Ctrl Pts',(109.402312464482,21.99325,32.8158271109875));
#106078=CARTESIAN_POINT('Ctrl Pts',(109.39630479516,21.99325,32.8215778437279));
#106079=CARTESIAN_POINT('Ctrl Pts',(109.390394923749,21.99325,32.8274241886413));
#106080=CARTESIAN_POINT('Ctrl Pts',(109.365023548343,21.99325,32.8525228415979));
#106081=CARTESIAN_POINT('Ctrl Pts',(109.341420589248,21.99325,32.8794095287664));
#106082=CARTESIAN_POINT('Ctrl Pts',(109.319661313854,21.99325,32.9078022118923));
#106083=CARTESIAN_POINT('Ctrl Pts',(109.303854012061,21.99325,32.9284284369287));
#106084=CARTESIAN_POINT('Ctrl Pts',(109.289019941609,21.99325,32.9498506817826));
#106085=CARTESIAN_POINT('Ctrl Pts',(109.27519572685,21.99325,32.9719757958513));
#106086=CARTESIAN_POINT('Ctrl Pts',(109.270957505281,21.99325,32.9787589034131));
#106087=CARTESIAN_POINT('Ctrl Pts',(109.266816302605,21.99325,32.985605032468));
#106088=CARTESIAN_POINT('Ctrl Pts',(109.262777145955,21.99325,32.9925040649077));
#106089=CARTESIAN_POINT('Ctrl Pts',(109.243693734176,21.99325,33.0250992545292));
#106090=CARTESIAN_POINT('Ctrl Pts',(109.22685695248,21.99325,33.0589177702548));
#106091=CARTESIAN_POINT('Ctrl Pts',(109.212348822142,21.99325,33.0936591021481));
#106092=CARTESIAN_POINT('Ctrl Pts',(109.197733505773,21.99325,33.1286571029161));
#106093=CARTESIAN_POINT('Ctrl Pts',(109.185480484964,21.99325,33.1645926511776));
#106094=CARTESIAN_POINT('Ctrl Pts',(109.175707331983,21.99325,33.2011997647515));
#106095=CARTESIAN_POINT('Ctrl Pts',(109.170688778414,21.99325,33.2199976655723));
#106096=CARTESIAN_POINT('Ctrl Pts',(109.166324758574,21.99325,33.2389732173444));
#106097=CARTESIAN_POINT('Ctrl Pts',(109.162635799128,21.99325,33.2580931624287));
#106098=CARTESIAN_POINT('Ctrl Pts',(109.160827961278,21.99325,33.2674632194669));
#106099=CARTESIAN_POINT('Ctrl Pts',(109.159182106796,21.99325,33.2768704544511));
#106100=CARTESIAN_POINT('Ctrl Pts',(109.157704090945,21.99325,33.2862874962798));
#106101=CARTESIAN_POINT('Ctrl Pts',(109.151655446475,21.99325,33.3248258772845));
#106102=CARTESIAN_POINT('Ctrl Pts',(109.148397359835,21.99325,33.3636070754909));
#106103=CARTESIAN_POINT('Ctrl Pts',(109.148031034507,21.99325,33.402343751128));
#106104=CARTESIAN_POINT('Ctrl Pts',(109.147673763903,21.99325,33.4401229447785));
#106105=CARTESIAN_POINT('Ctrl Pts',(109.150065954734,21.99325,33.4778610549384));
#106106=CARTESIAN_POINT('Ctrl Pts',(109.155030030729,21.99325,33.5153593431265));
#106107=CARTESIAN_POINT('Ctrl Pts',(109.157337041179,21.99325,33.5327863411743));
#106108=CARTESIAN_POINT('Ctrl Pts',(109.160200273373,21.99325,33.550161722503));
#106109=CARTESIAN_POINT('Ctrl Pts',(109.163605617005,21.99325,33.567466063713));
#106110=CARTESIAN_POINT('Ctrl Pts',(109.165348451527,21.99325,33.5763223221422));
#106111=CARTESIAN_POINT('Ctrl Pts',(109.167233319974,21.99325,33.585159974556));
#106112=CARTESIAN_POINT('Ctrl Pts',(109.16925855919,21.99325,33.5939764130428));
#106113=CARTESIAN_POINT('Ctrl Pts',(109.170862832037,21.99325,33.6009602659919));
#106114=CARTESIAN_POINT('Ctrl Pts',(109.172554757612,21.99325,33.6079285998806));
#106115=CARTESIAN_POINT('Ctrl Pts',(109.17433094191,21.99325,33.614871383303));
#106116=CARTESIAN_POINT('Ctrl Pts',(109.184136912542,21.99325,33.6532011503192));
#106117=CARTESIAN_POINT('Ctrl Pts',(109.19652383406,21.99325,33.6908270002868));
#106118=CARTESIAN_POINT('Ctrl Pts',(109.211283288827,21.99325,33.7275332573707));
#106119=CARTESIAN_POINT('Ctrl Pts',(109.226396659773,21.99325,33.7651196918364));
#106120=CARTESIAN_POINT('Ctrl Pts',(109.243997870408,21.99325,33.8017429878313));
#106121=CARTESIAN_POINT('Ctrl Pts',(109.263917687932,21.99325,33.8371751681065));
#106122=CARTESIAN_POINT('Ctrl Pts',(109.273277196623,21.99325,33.8538233024993));
#106123=CARTESIAN_POINT('Ctrl Pts',(109.283149334381,21.99325,33.8702084251205));
#106124=CARTESIAN_POINT('Ctrl Pts',(109.293520375918,21.99325,33.8863060632989));
#106125=CARTESIAN_POINT('Ctrl Pts',(109.299216111555,21.99325,33.8951468235169));
#106126=CARTESIAN_POINT('Ctrl Pts',(109.305062366064,21.99325,33.9039008597167));
#106127=CARTESIAN_POINT('Ctrl Pts',(109.311057158114,21.99325,33.9125639871748));
#106128=CARTESIAN_POINT('Ctrl Pts',(109.31565416963,21.99325,33.9192071695175));
#106129=CARTESIAN_POINT('Ctrl Pts',(109.320335637454,21.99325,33.9257925969553));
#106130=CARTESIAN_POINT('Ctrl Pts',(109.325095709211,21.99325,33.9323124342923));
#106131=CARTESIAN_POINT('Ctrl Pts',(109.350054193339,21.99325,33.9664978972433));
#106132=CARTESIAN_POINT('Ctrl Pts',(109.377205344832,21.99325,33.9989327926013));
#106133=CARTESIAN_POINT('Ctrl Pts',(109.406353139311,21.99325,34.0293791252897));
#106134=CARTESIAN_POINT('Ctrl Pts',(109.435309246376,21.99325,34.0596252308639));
#106135=CARTESIAN_POINT('Ctrl Pts',(109.466236355712,21.99325,34.0879100272063));
#106136=CARTESIAN_POINT('Ctrl Pts',(109.498989823094,21.99325,34.1139838486523));
#106137=CARTESIAN_POINT('Ctrl Pts',(109.523294998801,21.99325,34.1333322982136));
#106138=CARTESIAN_POINT('Ctrl Pts',(109.548606893583,21.99325,34.1514630223488));
#106139=CARTESIAN_POINT('Ctrl Pts',(109.574880871485,21.99325,34.1682622236805));
#106140=CARTESIAN_POINT('Ctrl Pts',(109.569164649808,21.99325,32.6980580125958));
#106141=CARTESIAN_POINT('Ctrl Pts',(109.753810436789,21.9736895721183,32.5674578367501));
#106142=CARTESIAN_POINT('Ctrl Pts',(110.273314592313,21.9329988322973,32.4811689689149));
#106143=CARTESIAN_POINT('Ctrl Pts',(110.840340273426,21.871177780537,33.0636201432557));
#106144=CARTESIAN_POINT('Ctrl Pts',(110.655412180794,21.8077868447193,33.8767425456563));
#106145=CARTESIAN_POINT('Ctrl Pts',(109.87248062677,21.7443959089015,34.1636192592745));
#106146=CARTESIAN_POINT('Ctrl Pts',(109.332505785412,21.6930427742276,33.7578415773765));
#106147=CARTESIAN_POINT('Ctrl Pts',(109.261694316903,21.662819951493,33.4061997065318));
#106148=CARTESIAN_POINT('Ctrl Pts',(109.262045097267,21.6537274406976,33.3002734582445));
#106149=CARTESIAN_POINT('Origin',(110.,21.99325,33.3));
#106150=CARTESIAN_POINT('',(109.03325,21.99325,33.3));
#106151=CARTESIAN_POINT('Origin',(110.,21.99325,33.3));
#106152=CARTESIAN_POINT('Origin',(110.,21.99325,33.3));
#106153=CARTESIAN_POINT('',(110.429877377952,21.99325,32.6988956497206));
#106154=CARTESIAN_POINT('Ctrl Pts',(110.426174626828,21.99325,34.1695497362103));
#106155=CARTESIAN_POINT('Ctrl Pts',(110.446294741806,21.99325,34.1568125013073));
#106156=CARTESIAN_POINT('Ctrl Pts',(110.465877499818,21.99325,34.14330064166));
#106157=CARTESIAN_POINT('Ctrl Pts',(110.484870687874,21.99325,34.1290117969353));
#106158=CARTESIAN_POINT('Ctrl Pts',(110.514960367498,21.99325,34.1063749042409));
#106159=CARTESIAN_POINT('Ctrl Pts',(110.54357182032,21.99325,34.081788511877));
#106160=CARTESIAN_POINT('Ctrl Pts',(110.570607330673,21.99325,34.0554521560241));
#106161=CARTESIAN_POINT('Ctrl Pts',(110.58591980247,21.99325,34.0405356739251));
#106162=CARTESIAN_POINT('Ctrl Pts',(110.600726220396,21.99325,34.0250574879875));
#106163=CARTESIAN_POINT('Ctrl Pts',(110.615004560658,21.99325,34.0090521485743));
#106164=CARTESIAN_POINT('Ctrl Pts',(110.621473282823,21.99325,34.0018010191072));
#106165=CARTESIAN_POINT('Ctrl Pts',(110.627832369673,21.99325,33.9944428472011));
#106166=CARTESIAN_POINT('Ctrl Pts',(110.63407242037,21.99325,33.9869901381755));
#106167=CARTESIAN_POINT('Ctrl Pts',(110.660863661377,21.99325,33.9549924296047));
#106168=CARTESIAN_POINT('Ctrl Pts',(110.685505043446,21.99325,33.9212086657911));
#106169=CARTESIAN_POINT('Ctrl Pts',(110.707856824131,21.99325,33.8859124195861));
#106170=CARTESIAN_POINT('Ctrl Pts',(110.720728374224,21.99325,33.8655866384995));
#106171=CARTESIAN_POINT('Ctrl Pts',(110.732839764501,21.99325,33.8447589036181));
#106172=CARTESIAN_POINT('Ctrl Pts',(110.74415655274,21.99325,33.8234800396049));
#106173=CARTESIAN_POINT('Ctrl Pts',(110.748940610787,21.99325,33.8144846145377));
#106174=CARTESIAN_POINT('Ctrl Pts',(110.753582593749,21.99325,33.8054085665864));
#106175=CARTESIAN_POINT('Ctrl Pts',(110.75807957408,21.99325,33.7962557496567));
#106176=CARTESIAN_POINT('Ctrl Pts',(110.761770866658,21.99325,33.7887427692294));
#106177=CARTESIAN_POINT('Ctrl Pts',(110.765360254662,21.99325,33.7811866076814));
#106178=CARTESIAN_POINT('Ctrl Pts',(110.768846556029,21.99325,33.7735900770095));
#106179=CARTESIAN_POINT('Ctrl Pts',(110.785569298044,21.99325,33.7371517977927));
#106180=CARTESIAN_POINT('Ctrl Pts',(110.79992620115,21.99325,33.6997811388704));
#106181=CARTESIAN_POINT('Ctrl Pts',(110.811786822027,21.99325,33.6617216338423));
#106182=CARTESIAN_POINT('Ctrl Pts',(110.823370425106,21.99325,33.6245510502608));
#106183=CARTESIAN_POINT('Ctrl Pts',(110.83257307252,21.99325,33.5867223451475));
#106184=CARTESIAN_POINT('Ctrl Pts',(110.839225035118,21.99325,33.54846478224));
#106185=CARTESIAN_POINT('Ctrl Pts',(110.842386440096,21.99325,33.5302825318116));
#106186=CARTESIAN_POINT('Ctrl Pts',(110.844970999637,21.99325,33.5120035489813));
#106187=CARTESIAN_POINT('Ctrl Pts',(110.846956463004,21.99325,33.4936536749133));
#106188=CARTESIAN_POINT('Ctrl Pts',(110.847833192143,21.99325,33.4855508463484));
#106189=CARTESIAN_POINT('Ctrl Pts',(110.848593070033,21.99325,33.4774342090572));
#106190=CARTESIAN_POINT('Ctrl Pts',(110.849234013381,21.99325,33.4693060637584));
#106191=CARTESIAN_POINT('Ctrl Pts',(110.849865427658,21.99325,33.4612987617171));
#106192=CARTESIAN_POINT('Ctrl Pts',(110.850380715277,21.99325,33.45328873078));
#106193=CARTESIAN_POINT('Ctrl Pts',(110.850778455272,21.99325,33.4452818304454));
#106194=CARTESIAN_POINT('Ctrl Pts',(110.852542333712,21.99325,33.4097732091587));
#106195=CARTESIAN_POINT('Ctrl Pts',(110.851999556645,21.99325,33.3743011239417));
#106196=CARTESIAN_POINT('Ctrl Pts',(110.849028272475,21.99325,33.3390457962148));
#106197=CARTESIAN_POINT('Ctrl Pts',(110.846251958068,21.99325,33.3061038530315));
#106198=CARTESIAN_POINT('Ctrl Pts',(110.841354467676,21.99325,33.2733506949589));
#106199=CARTESIAN_POINT('Ctrl Pts',(110.834425817615,21.99325,33.2409490348578));
#106200=CARTESIAN_POINT('Ctrl Pts',(110.830911409544,21.99325,33.224513992715));
#106201=CARTESIAN_POINT('Ctrl Pts',(110.826874028556,21.99325,33.2081696208379));
#106202=CARTESIAN_POINT('Ctrl Pts',(110.82232328327,21.99325,33.1919389686854));
#106203=CARTESIAN_POINT('Ctrl Pts',(110.819274840855,21.99325,33.1810664180728));
#106204=CARTESIAN_POINT('Ctrl Pts',(110.815996005313,21.99325,33.1702449246969));
#106205=CARTESIAN_POINT('Ctrl Pts',(110.812489369983,21.99325,33.1594818015797));
#106206=CARTESIAN_POINT('Ctrl Pts',(110.809585252903,21.99325,33.1505680233467));
#106207=CARTESIAN_POINT('Ctrl Pts',(110.806523937818,21.99325,33.1416922065324));
#106208=CARTESIAN_POINT('Ctrl Pts',(110.803315104313,21.99325,33.1328799180716));
#106209=CARTESIAN_POINT('Ctrl Pts',(110.790547715166,21.99325,33.0978173584587));
#106210=CARTESIAN_POINT('Ctrl Pts',(110.775425302369,21.99325,33.0636827746753));
#106211=CARTESIAN_POINT('Ctrl Pts',(110.758092822638,21.99325,33.0307063318292));
#106212=CARTESIAN_POINT('Ctrl Pts',(110.740958075622,21.99325,32.9981060914485));
#106213=CARTESIAN_POINT('Ctrl Pts',(110.721662428768,21.99325,32.9666368288481));
#106214=CARTESIAN_POINT('Ctrl Pts',(110.700313079278,21.99325,32.9365590456047));
#106215=CARTESIAN_POINT('Ctrl Pts',(110.690673858058,21.99325,32.9229789406643));
#106216=CARTESIAN_POINT('Ctrl Pts',(110.680615626106,21.99325,32.9096830911525));
#106217=CARTESIAN_POINT('Ctrl Pts',(110.670146809868,21.99325,32.8966987819899));
#106218=CARTESIAN_POINT('Ctrl Pts',(110.665276843094,21.99325,32.8906586383129));
#106219=CARTESIAN_POINT('Ctrl Pts',(110.660316746254,21.99325,32.884684463972));
#106220=CARTESIAN_POINT('Ctrl Pts',(110.655271360203,21.99325,32.8787838850441));
#106221=CARTESIAN_POINT('Ctrl Pts',(110.632244741213,21.99325,32.8518542544048));
#106222=CARTESIAN_POINT('Ctrl Pts',(110.607540668324,21.99325,32.8265654533201));
#106223=CARTESIAN_POINT('Ctrl Pts',(110.581270482762,21.99325,32.8031360739611));
#106224=CARTESIAN_POINT('Ctrl Pts',(110.555959181703,21.99325,32.78056188722));
#106225=CARTESIAN_POINT('Ctrl Pts',(110.529193139856,21.99325,32.7597134486046));
#106226=CARTESIAN_POINT('Ctrl Pts',(110.501054523868,21.99325,32.7408301544696));
#106227=CARTESIAN_POINT('Ctrl Pts',(110.478219674726,21.99325,32.7255061181679));
#106228=CARTESIAN_POINT('Ctrl Pts',(110.454480437898,21.99325,32.7114769174597));
#106229=CARTESIAN_POINT('Ctrl Pts',(110.429877377952,21.99325,32.6988956497206));
#106230=CARTESIAN_POINT('Origin',(110.,21.99325,33.3));
#106231=CARTESIAN_POINT('Origin',(110.,22.7327725593024,33.3));
#106232=CARTESIAN_POINT('Ctrl Pts',(110.429877377952,21.99325,32.6988956497206));
#106233=CARTESIAN_POINT('Ctrl Pts',(110.629392425721,21.9721196880608,32.8415780401524));
#106234=CARTESIAN_POINT('Ctrl Pts',(110.871460562011,21.9298590641823,33.3393357713752));
#106235=CARTESIAN_POINT('Ctrl Pts',(110.441011075278,21.8664681283645,34.0539278279709));
#106236=CARTESIAN_POINT('Ctrl Pts',(109.60727954107,21.8030771925468,34.079572693842));
#106237=CARTESIAN_POINT('Ctrl Pts',(109.273287397513,21.7585120028594,33.5980922637393));
#106238=CARTESIAN_POINT('Ctrl Pts',(109.259905511347,21.7350771251113,33.3271351273468));
#106239=CARTESIAN_POINT('Ctrl Pts',(109.260096259818,21.7327725593024,33.3004698838673));
#106240=CARTESIAN_POINT('Ctrl Pts',(110.562359885163,22.1247415238079,32.5136432603077));
#106241=CARTESIAN_POINT('Ctrl Pts',(110.823362824852,22.1036112118687,32.7002984713361));
#106242=CARTESIAN_POINT('Ctrl Pts',(111.140033150641,22.0613505879902,33.3514585344749));
#106243=CARTESIAN_POINT('Ctrl Pts',(110.576924840359,21.9979596521725,34.2862783865912));
#106244=CARTESIAN_POINT('Ctrl Pts',(109.486248303559,21.9345687163548,34.3198266600429));
#106245=CARTESIAN_POINT('Ctrl Pts',(108.864753649643,21.871177780537,33.4238848870208));
#106246=CARTESIAN_POINT('Ctrl Pts',(109.278620310884,21.8077868447193,32.4145625088781));
#106247=CARTESIAN_POINT('Ctrl Pts',(110.350675199839,21.7443959089015,32.2131476509265));
#106248=CARTESIAN_POINT('Ctrl Pts',(111.102775091905,21.6810049730838,33.0031216845332));
#106249=CARTESIAN_POINT('Ctrl Pts',(110.84890495161,21.6176140372661,34.0639581186772));
#106250=CARTESIAN_POINT('Ctrl Pts',(109.820617769302,21.5542231014483,34.4278636578058));
#106251=CARTESIAN_POINT('Ctrl Pts',(108.955975747213,21.4908321656306,33.7628948884635));
#106252=CARTESIAN_POINT('Ctrl Pts',(109.043732049669,21.4274412298128,32.6756514155529));
#106253=CARTESIAN_POINT('Ctrl Pts',(110.003835112584,21.3640502939951,32.1579646066592));
#106254=CARTESIAN_POINT('Ctrl Pts',(110.960439907255,21.3006593581774,32.6820894055575));
#106255=CARTESIAN_POINT('Ctrl Pts',(111.040891398074,21.2372684223596,33.7698930864614));
#106256=CARTESIAN_POINT('Ctrl Pts',(110.171803802845,21.1738774865419,34.4290505202554));
#106257=CARTESIAN_POINT('Ctrl Pts',(109.145981672175,21.1104865507242,34.0582231421285));
#106258=CARTESIAN_POINT('Ctrl Pts',(108.899247052897,21.0470956149064,32.9957565548576));
#106259=CARTESIAN_POINT('Ctrl Pts',(109.65662563213,20.9837046790887,32.2107423399201));
#106260=CARTESIAN_POINT('Ctrl Pts',(110.727326917525,20.920313743271,32.4195868604602));
#106261=CARTESIAN_POINT('Ctrl Pts',(111.134364726985,20.8569228074532,33.4311635936655));
#106262=CARTESIAN_POINT('Ctrl Pts',(110.507004538604,20.7935318716355,34.3239793577582));
#106263=CARTESIAN_POINT('Ctrl Pts',(109.416540606268,20.7301409358177,34.2807643453944));
#106264=CARTESIAN_POINT('Ctrl Pts',(109.046513639301,20.6878803119393,33.6583741407962));
#106265=CARTESIAN_POINT('Ctrl Pts',(109.033986956687,20.66675,33.3377407293226));
#106266=CARTESIAN_POINT('Ctrl Pts',(110.518199049426,22.080911015872,32.5753940567787));
#106267=CARTESIAN_POINT('Ctrl Pts',(110.758706025142,22.0597807039327,32.7473916609415));
#106268=CARTESIAN_POINT('Ctrl Pts',(111.050508954431,22.0175200800542,33.3474176134417));
#106269=CARTESIAN_POINT('Ctrl Pts',(110.531620251999,21.9541291442365,34.2088282003844));
#106270=CARTESIAN_POINT('Ctrl Pts',(109.526592049396,21.8907382084188,34.2397420046426));
#106271=CARTESIAN_POINT('Ctrl Pts',(108.953901949374,21.827347272601,33.4141564901519));
#106272=CARTESIAN_POINT('Ctrl Pts',(109.335268608168,21.7639563367833,32.4840938901739));
#106273=CARTESIAN_POINT('Ctrl Pts',(110.323137478345,21.7005654009656,32.2984956804072));
#106274=CARTESIAN_POINT('Ctrl Pts',(111.016176685843,21.6371744651478,33.0264348597242));
#106275=CARTESIAN_POINT('Ctrl Pts',(110.782242387097,21.5737835293301,34.0039662346917));
#106276=CARTESIAN_POINT('Ctrl Pts',(109.834704245655,21.5103925935123,34.3392951040379));
#106277=CARTESIAN_POINT('Ctrl Pts',(109.037960584235,21.4470016576946,33.7265448114537));
#106278=CARTESIAN_POINT('Ctrl Pts',(109.118825584946,21.3836107218769,32.7246800820843));
#106279=CARTESIAN_POINT('Ctrl Pts',(110.003533949963,21.3202197860591,32.2476460344097));
#106280=CARTESIAN_POINT('Ctrl Pts',(110.885018757741,21.2568288502414,32.7306125114567));
#106281=CARTESIAN_POINT('Ctrl Pts',(110.959152576969,21.1934379144237,33.7329934569668));
#106282=CARTESIAN_POINT('Ctrl Pts',(110.158312443101,21.1300469786059,34.3403887648936));
#106283=CARTESIAN_POINT('Ctrl Pts',(109.213045778429,21.0666560427882,33.9986816127363));
#106284=CARTESIAN_POINT('Ctrl Pts',(108.985686664552,21.0032651069704,33.0196480968388));
#106285=CARTESIAN_POINT('Ctrl Pts',(109.683590035986,20.9398741711527,32.2962792529735));
#106286=CARTESIAN_POINT('Ctrl Pts',(110.670211597996,20.876483235335,32.4887236909162));
#106287=CARTESIAN_POINT('Ctrl Pts',(111.045285659121,20.8130922995172,33.4208636166092));
#106288=CARTESIAN_POINT('Ctrl Pts',(110.467190631642,20.7497013636995,34.243568600503));
#106289=CARTESIAN_POINT('Ctrl Pts',(109.46235833816,20.6863104278818,34.2037471642329));
#106290=CARTESIAN_POINT('Ctrl Pts',(109.121388742706,20.6440498040033,33.6302318390752));
#106291=CARTESIAN_POINT('Ctrl Pts',(109.109845751831,20.622919492064,33.3347770361571));
#106292=CARTESIAN_POINT('Ctrl Pts',(110.474038213689,22.037080507936,32.6371448532496));
#106293=CARTESIAN_POINT('Ctrl Pts',(110.694049225431,22.0159501959967,32.794484850547));
#106294=CARTESIAN_POINT('Ctrl Pts',(110.960984758221,21.9736895721183,33.3433766924084));
#106295=CARTESIAN_POINT('Ctrl Pts',(110.486315663638,21.9102986363005,34.1313780141776));
#106296=CARTESIAN_POINT('Ctrl Pts',(109.566935795233,21.8469077004828,34.1596573492423));
#106297=CARTESIAN_POINT('Ctrl Pts',(109.043050249104,21.783516764665,33.404428093283));
#106298=CARTESIAN_POINT('Ctrl Pts',(109.391916905451,21.7201258288473,32.5536252714697));
#106299=CARTESIAN_POINT('Ctrl Pts',(110.295599756851,21.6567348930296,32.383843709888));
#106300=CARTESIAN_POINT('Ctrl Pts',(110.929578279781,21.5933439572118,33.0497480349151));
#106301=CARTESIAN_POINT('Ctrl Pts',(110.715579822584,21.5299530213941,33.9439743507063));
#106302=CARTESIAN_POINT('Ctrl Pts',(109.848790722007,21.4665620855764,34.25072655027));
#106303=CARTESIAN_POINT('Ctrl Pts',(109.119945421257,21.4031711497586,33.6901947344439));
#106304=CARTESIAN_POINT('Ctrl Pts',(109.193919120223,21.3397802139409,32.7737087486158));
#106305=CARTESIAN_POINT('Ctrl Pts',(110.003232787343,21.2763892781232,32.3373274621601));
#106306=CARTESIAN_POINT('Ctrl Pts',(110.809597608227,21.2129983423054,32.779135617356));
#106307=CARTESIAN_POINT('Ctrl Pts',(110.877413755863,21.1496074064877,33.6960938274722));
#106308=CARTESIAN_POINT('Ctrl Pts',(110.144821083357,21.0862164706699,34.2517270095317));
#106309=CARTESIAN_POINT('Ctrl Pts',(109.280109884683,21.0228255348522,33.9391400833441));
#106310=CARTESIAN_POINT('Ctrl Pts',(109.072126276207,20.9594345990345,33.0435396388201));
#106311=CARTESIAN_POINT('Ctrl Pts',(109.710554439841,20.8960436632167,32.381816166027));
#106312=CARTESIAN_POINT('Ctrl Pts',(110.613096278466,20.832652727399,32.5578605213723));
#106313=CARTESIAN_POINT('Ctrl Pts',(110.956206591258,20.7692617915813,33.410563639553));
#106314=CARTESIAN_POINT('Ctrl Pts',(110.427376724679,20.7058708557635,34.1631578432478));
#106315=CARTESIAN_POINT('Ctrl Pts',(109.508176070054,20.6424799199458,34.1267299830714));
#106316=CARTESIAN_POINT('Ctrl Pts',(109.19626384611,20.6002192960673,33.6020895373542));
#106317=CARTESIAN_POINT('Ctrl Pts',(109.185704546974,20.5790889841281,33.3318133429916));
#106318=CARTESIAN_POINT('Ctrl Pts',(110.429877377952,21.99325,32.6988956497206));
#106319=CARTESIAN_POINT('Ctrl Pts',(110.629392425721,21.9721196880608,32.8415780401524));
#106320=CARTESIAN_POINT('Ctrl Pts',(110.871460562011,21.9298590641823,33.3393357713752));
#106321=CARTESIAN_POINT('Ctrl Pts',(110.441011075278,21.8664681283645,34.0539278279709));
#106322=CARTESIAN_POINT('Ctrl Pts',(109.60727954107,21.8030771925468,34.079572693842));
#106323=CARTESIAN_POINT('Ctrl Pts',(109.132198548835,21.7396862567291,33.3946996964141));
#106324=CARTESIAN_POINT('Ctrl Pts',(109.448565202734,21.6762953209113,32.6231566527654));
#106325=CARTESIAN_POINT('Ctrl Pts',(110.268062035357,21.6129043850936,32.4691917393687));
#106326=CARTESIAN_POINT('Ctrl Pts',(110.842979873719,21.5495134492758,33.0730612101061));
#106327=CARTESIAN_POINT('Ctrl Pts',(110.648917258071,21.4861225134581,33.8839824667209));
#106328=CARTESIAN_POINT('Ctrl Pts',(109.86287719836,21.4227315776404,34.1621579965021));
#106329=CARTESIAN_POINT('Ctrl Pts',(109.201930258278,21.3593406418226,33.6538446574342));
#106330=CARTESIAN_POINT('Ctrl Pts',(109.269012655501,21.2959497060049,32.8227374151472));
#106331=CARTESIAN_POINT('Ctrl Pts',(110.002931624722,21.2325587701872,32.4270088899107));
#106332=CARTESIAN_POINT('Ctrl Pts',(110.734176458714,21.1691678343694,32.8276587232552));
#106333=CARTESIAN_POINT('Ctrl Pts',(110.795674934758,21.1057768985517,33.6591941979777));
#106334=CARTESIAN_POINT('Ctrl Pts',(110.131329723613,21.042385962734,34.1630652541699));
#106335=CARTESIAN_POINT('Ctrl Pts',(109.347173990936,20.9789950269162,33.8795985539519));
#106336=CARTESIAN_POINT('Ctrl Pts',(109.158565887862,20.9156040910985,33.0674311808014));
#106337=CARTESIAN_POINT('Ctrl Pts',(109.737518843697,20.8522131552808,32.4673530790804));
#106338=CARTESIAN_POINT('Ctrl Pts',(110.555980958936,20.788822219463,32.6269973518284));
#106339=CARTESIAN_POINT('Ctrl Pts',(110.867127523395,20.7254312836453,33.4002636624968));
#106340=CARTESIAN_POINT('Ctrl Pts',(110.387562817717,20.6620403478275,34.0827470859926));
#106341=CARTESIAN_POINT('Ctrl Pts',(109.553993801946,20.5986494120098,34.04971280191));
#106342=CARTESIAN_POINT('Ctrl Pts',(109.271138949515,20.5563887881313,33.5739472356332));
#106343=CARTESIAN_POINT('Ctrl Pts',(109.261563342117,20.5352584761921,33.3288496498261));
#106344=CARTESIAN_POINT('Origin',(110.,22.1,33.3));
#106345=CARTESIAN_POINT('',(109.330384757729,22.2,33.3));
#106346=CARTESIAN_POINT('Origin',(110.,22.2,33.3));
#106347=CARTESIAN_POINT('',(109.480384757729,22.05,33.3));
#106348=CARTESIAN_POINT('',(109.430384757729,22.1,33.3));
#106349=CARTESIAN_POINT('',(109.543134871874,22.,33.1913136141202));
#106350=CARTESIAN_POINT('Ctrl Pts',(109.543134871874,22.,33.1913136141202));
#106351=CARTESIAN_POINT('Ctrl Pts',(109.513345646292,22.0170391114376,33.2429100663472));
#106352=CARTESIAN_POINT('Ctrl Pts',(109.480384757729,22.05,33.3));
#106353=CARTESIAN_POINT('',(109.67744226472,22.,32.9586863858798));
#106354=CARTESIAN_POINT('Origin',(110.,22.,33.3));
#106355=CARTESIAN_POINT('',(109.740192378865,22.05,32.85));
#106356=CARTESIAN_POINT('Ctrl Pts',(109.740192378865,22.05,32.85));
#106357=CARTESIAN_POINT('Ctrl Pts',(109.707231490302,22.0170391114376,32.9070899336529));
#106358=CARTESIAN_POINT('Ctrl Pts',(109.67744226472,22.,32.9586863858798));
#106359=CARTESIAN_POINT('',(109.865692607155,22.,32.85));
#106360=CARTESIAN_POINT('Ctrl Pts',(109.865692607155,22.,32.85));
#106361=CARTESIAN_POINT('Ctrl Pts',(109.80611415599,22.0170391114376,32.85));
#106362=CARTESIAN_POINT('Ctrl Pts',(109.740192378865,22.05,32.85));
#106363=CARTESIAN_POINT('',(110.134307392845,22.,32.85));
#106364=CARTESIAN_POINT('Origin',(110.,22.,33.3));
#106365=CARTESIAN_POINT('',(110.259807621135,22.05,32.85));
#106366=CARTESIAN_POINT('Ctrl Pts',(110.259807621135,22.05,32.85));
#106367=CARTESIAN_POINT('Ctrl Pts',(110.19388584401,22.0170391114376,32.85));
#106368=CARTESIAN_POINT('Ctrl Pts',(110.134307392845,22.,32.85));
#106369=CARTESIAN_POINT('',(110.32255773528,22.,32.9586863858798));
#106370=CARTESIAN_POINT('Ctrl Pts',(110.32255773528,22.,32.9586863858798));
#106371=CARTESIAN_POINT('Ctrl Pts',(110.292768509698,22.0170391114376,32.9070899336528));
#106372=CARTESIAN_POINT('Ctrl Pts',(110.259807621135,22.05,32.85));
#106373=CARTESIAN_POINT('',(110.456865128126,22.,33.1913136141202));
#106374=CARTESIAN_POINT('Origin',(110.,22.,33.3));
#106375=CARTESIAN_POINT('',(110.519615242271,22.05,33.3));
#106376=CARTESIAN_POINT('Ctrl Pts',(110.519615242271,22.05,33.3));
#106377=CARTESIAN_POINT('Ctrl Pts',(110.486654353708,22.0170391114376,33.2429100663471));
#106378=CARTESIAN_POINT('Ctrl Pts',(110.456865128126,22.,33.1913136141202));
#106379=CARTESIAN_POINT('',(110.456865128126,22.,33.4086863858798));
#106380=CARTESIAN_POINT('Ctrl Pts',(110.456865128126,22.,33.4086863858798));
#106381=CARTESIAN_POINT('Ctrl Pts',(110.486654353708,22.0170391114376,33.3570899336528));
#106382=CARTESIAN_POINT('Ctrl Pts',(110.519615242271,22.05,33.3));
#106383=CARTESIAN_POINT('',(110.32255773528,22.,33.6413136141202));
#106384=CARTESIAN_POINT('Origin',(110.,22.,33.3));
#106385=CARTESIAN_POINT('',(110.259807621135,22.05,33.75));
#106386=CARTESIAN_POINT('Ctrl Pts',(110.259807621135,22.05,33.75));
#106387=CARTESIAN_POINT('Ctrl Pts',(110.292768509698,22.0170391114376,33.6929100663471));
#106388=CARTESIAN_POINT('Ctrl Pts',(110.32255773528,22.,33.6413136141202));
#106389=CARTESIAN_POINT('',(110.134307392845,22.,33.75));
#106390=CARTESIAN_POINT('Ctrl Pts',(110.134307392845,22.,33.75));
#106391=CARTESIAN_POINT('Ctrl Pts',(110.19388584401,22.0170391114376,33.75));
#106392=CARTESIAN_POINT('Ctrl Pts',(110.259807621135,22.05,33.75));
#106393=CARTESIAN_POINT('',(109.865692607155,22.,33.75));
#106394=CARTESIAN_POINT('Origin',(110.,22.,33.3));
#106395=CARTESIAN_POINT('',(109.740192378865,22.05,33.75));
#106396=CARTESIAN_POINT('Ctrl Pts',(109.740192378865,22.05,33.75));
#106397=CARTESIAN_POINT('Ctrl Pts',(109.80611415599,22.0170391114376,33.75));
#106398=CARTESIAN_POINT('Ctrl Pts',(109.865692607155,22.,33.75));
#106399=CARTESIAN_POINT('',(109.67744226472,22.,33.6413136141202));
#106400=CARTESIAN_POINT('Ctrl Pts',(109.67744226472,22.,33.6413136141202));
#106401=CARTESIAN_POINT('Ctrl Pts',(109.707231490302,22.0170391114376,33.6929100663472));
#106402=CARTESIAN_POINT('Ctrl Pts',(109.740192378865,22.05,33.75));
#106403=CARTESIAN_POINT('',(109.543134871874,22.,33.4086863858798));
#106404=CARTESIAN_POINT('Origin',(110.,22.,33.3));
#106405=CARTESIAN_POINT('Ctrl Pts',(109.480384757729,22.05,33.3));
#106406=CARTESIAN_POINT('Ctrl Pts',(109.513345646292,22.0170391114376,33.3570899336529));
#106407=CARTESIAN_POINT('Ctrl Pts',(109.543134871874,22.,33.4086863858798));
#106408=CARTESIAN_POINT('Origin',(110.,22.1,33.3));
#106409=CARTESIAN_POINT('',(110.134307392845,22.2,32.85));
#106410=CARTESIAN_POINT('',(110.134307392845,22.1,32.85));
#106411=CARTESIAN_POINT('',(109.865692607155,22.2,32.85));
#106412=CARTESIAN_POINT('',(109.865692607155,22.1,32.85));
#106413=CARTESIAN_POINT('Origin',(110.,22.2,33.3));
#106414=CARTESIAN_POINT('Origin',(110.,22.1,33.3));
#106415=CARTESIAN_POINT('',(110.456865128126,22.2,33.1913136141202));
#106416=CARTESIAN_POINT('',(110.456865128126,22.1,33.1913136141202));
#106417=CARTESIAN_POINT('',(110.32255773528,22.2,32.9586863858798));
#106418=CARTESIAN_POINT('',(110.32255773528,22.1,32.9586863858798));
#106419=CARTESIAN_POINT('Origin',(110.,22.2,33.3));
#106420=CARTESIAN_POINT('Origin',(110.,22.1,33.3));
#106421=CARTESIAN_POINT('',(109.543134871874,22.2,33.1913136141202));
#106422=CARTESIAN_POINT('',(109.543134871874,22.1,33.1913136141202));
#106423=CARTESIAN_POINT('',(109.67744226472,22.2,32.9586863858798));
#106424=CARTESIAN_POINT('Origin',(110.,22.2,33.3));
#106425=CARTESIAN_POINT('',(109.67744226472,22.1,32.9586863858798));
#106426=CARTESIAN_POINT('Origin',(110.,22.1,33.3));
#106427=CARTESIAN_POINT('',(110.32255773528,22.2,33.6413136141202));
#106428=CARTESIAN_POINT('',(110.32255773528,22.1,33.6413136141202));
#106429=CARTESIAN_POINT('',(110.456865128126,22.2,33.4086863858798));
#106430=CARTESIAN_POINT('',(110.456865128126,22.1,33.4086863858798));
#106431=CARTESIAN_POINT('Origin',(110.,22.2,33.3));
#106432=CARTESIAN_POINT('Origin',(110.,22.1,33.3));
#106433=CARTESIAN_POINT('',(109.67744226472,22.2,33.6413136141202));
#106434=CARTESIAN_POINT('',(109.67744226472,22.1,33.6413136141202));
#106435=CARTESIAN_POINT('',(109.543134871874,22.2,33.4086863858798));
#106436=CARTESIAN_POINT('Origin',(110.,22.2,33.3));
#106437=CARTESIAN_POINT('',(109.543134871874,22.1,33.4086863858798));
#106438=CARTESIAN_POINT('Origin',(110.,22.1,33.3));
#106439=CARTESIAN_POINT('',(110.134307392845,22.2,33.75));
#106440=CARTESIAN_POINT('',(110.134307392845,22.1,33.75));
#106441=CARTESIAN_POINT('',(109.865692607155,22.2,33.75));
#106442=CARTESIAN_POINT('Origin',(110.,22.2,33.3));
#106443=CARTESIAN_POINT('',(109.865692607155,22.1,33.75));
#106444=CARTESIAN_POINT('Origin',(110.519615242271,22.2,33.3));
#106445=CARTESIAN_POINT('',(110.549663336987,22.2,33.247955173281));
#106446=CARTESIAN_POINT('',(110.519615242271,21.4,33.3));
#106447=CARTESIAN_POINT('',(110.519615242271,22.2,33.3));
#106448=CARTESIAN_POINT('',(110.259807621135,21.4,33.75));
#106449=CARTESIAN_POINT('',(110.519615242271,21.4,33.3));
#106450=CARTESIAN_POINT('',(110.259807621135,22.2,33.75));
#106451=CARTESIAN_POINT('Origin',(110.259807621135,22.2,32.85));
#106452=CARTESIAN_POINT('',(110.419759526419,22.2,33.127044826719));
#106453=CARTESIAN_POINT('',(110.259807621135,21.4,32.85));
#106454=CARTESIAN_POINT('',(110.259807621135,22.2,32.85));
#106455=CARTESIAN_POINT('',(110.259807621135,21.4,32.85));
#106456=CARTESIAN_POINT('Origin',(109.740192378865,22.2,32.85));
#106457=CARTESIAN_POINT('',(110.250096189432,22.2,32.85));
#106458=CARTESIAN_POINT('',(109.740192378865,21.4,32.85));
#106459=CARTESIAN_POINT('',(109.740192378865,22.2,32.85));
#106460=CARTESIAN_POINT('',(109.740192378865,21.4,32.85));
#106461=CARTESIAN_POINT('Origin',(110.76,22.2,33.3));
#106462=CARTESIAN_POINT('Origin',(110.76,22.2,33.3));
#106463=CARTESIAN_POINT('Origin',(110.76,22.2,33.3));
#106464=CARTESIAN_POINT('',(109.640336663013,22.2,33.022955173281));
#106465=CARTESIAN_POINT('Origin',(110.76,22.2,33.3));
#106466=CARTESIAN_POINT('Origin',(110.76,22.2,33.3));
#106467=CARTESIAN_POINT('',(109.770240473581,22.2,33.802044826719));
#106468=CARTESIAN_POINT('Origin',(110.76,22.2,33.3));
#106469=CARTESIAN_POINT('',(110.509903810568,22.2,33.75));
#106470=CARTESIAN_POINT('Origin',(110.519615242271,21.4,33.3));
#106471=CARTESIAN_POINT('',(109.480384757729,21.4,33.3));
#106472=CARTESIAN_POINT('',(109.480384757729,21.4,33.3));
#106473=CARTESIAN_POINT('Origin',(110.,21.4,33.3));
#106474=CARTESIAN_POINT('Origin',(110.519615242271,21.4,33.3));
#106475=CARTESIAN_POINT('Origin',(110.,21.4,33.3));
#106476=CARTESIAN_POINT('Origin',(110.519615242271,21.4,33.3));
#106477=CARTESIAN_POINT('Origin',(110.,21.4,33.3));
#106478=CARTESIAN_POINT('Origin',(110.519615242271,21.4,33.3));
#106479=CARTESIAN_POINT('Origin',(110.,21.4,33.3));
#106480=CARTESIAN_POINT('Origin',(110.519615242271,21.4,33.3));
#106481=CARTESIAN_POINT('',(109.740192378865,21.4,33.75));
#106482=CARTESIAN_POINT('',(110.259807621135,21.4,33.75));
#106483=CARTESIAN_POINT('Origin',(110.,21.4,33.3));
#106484=CARTESIAN_POINT('Origin',(110.519615242271,21.4,33.3));
#106485=CARTESIAN_POINT('',(109.740192378865,21.4,33.75));
#106486=CARTESIAN_POINT('Origin',(110.,21.4,33.3));
#106487=CARTESIAN_POINT('Origin',(110.,21.4,33.3));
#106488=CARTESIAN_POINT('',(110.,21.0877836638731,33.3));
#106489=CARTESIAN_POINT('',(109.480384757729,21.4,33.3));
#106490=CARTESIAN_POINT('Origin',(109.480384757729,22.2,33.3));
#106491=CARTESIAN_POINT('',(109.480384757729,22.2,33.3));
#106492=CARTESIAN_POINT('Origin',(109.740192378865,22.2,33.75));
#106493=CARTESIAN_POINT('',(109.740192378865,22.2,33.75));
#106494=CARTESIAN_POINT('Origin',(110.259807621135,22.2,33.75));
#106495=CARTESIAN_POINT('Origin',(110.76,22.2,33.3));
#106496=CARTESIAN_POINT('',(109.24,22.2,33.3));
#106497=CARTESIAN_POINT('Origin',(110.,22.2,33.3));
#106498=CARTESIAN_POINT('Origin',(110.,22.08,33.3));
#106499=CARTESIAN_POINT('',(109.12,22.08,33.3));
#106500=CARTESIAN_POINT('Origin',(110.,21.33,33.3));
#106501=CARTESIAN_POINT('Origin',(110.,20.66675,33.3));
#106502=CARTESIAN_POINT('Origin',(110.,20.45,33.3));
#106503=CARTESIAN_POINT('',(109.5,20.2,33.3));
#106504=CARTESIAN_POINT('Origin',(110.,20.2,33.3));
#106505=CARTESIAN_POINT('',(109.25,20.45,33.3));
#106506=CARTESIAN_POINT('Origin',(110.,20.2,33.3));
#113958=UNCERTAINTY_MEASURE_WITH_UNIT(LENGTH_MEASURE(0.01),#113985,
'DISTANCE_ACCURACY_VALUE',
'Maximum model space distance between geometric entities at asserted c
onnectivities');
#113964=UNCERTAINTY_MEASURE_WITH_UNIT(LENGTH_MEASURE(0.01),#113985,
'DISTANCE_ACCURACY_VALUE',
'Maximum model space distance between geometric entities at asserted c
onnectivities');
#113978=(
GEOMETRIC_REPRESENTATION_CONTEXT(3)
GLOBAL_UNCERTAINTY_ASSIGNED_CONTEXT((#113958))
GLOBAL_UNIT_ASSIGNED_CONTEXT((#113985,#113987,#113988))
REPRESENTATION_CONTEXT('','3D')
);
#113984=(
GEOMETRIC_REPRESENTATION_CONTEXT(3)
GLOBAL_UNCERTAINTY_ASSIGNED_CONTEXT((#113964))
GLOBAL_UNIT_ASSIGNED_CONTEXT((#113985,#113987,#113988))
REPRESENTATION_CONTEXT('','3D')
);
#113985=(
LENGTH_UNIT()
NAMED_UNIT(*)
SI_UNIT(.MILLI.,.METRE.)
);
#113987=(
NAMED_UNIT(*)
PLANE_ANGLE_UNIT()
SI_UNIT($,.RADIAN.)
);
#113988=(
NAMED_UNIT(*)
SI_UNIT($,.STERADIAN.)
SOLID_ANGLE_UNIT()
);
#114002=SHAPE_DEFINITION_REPRESENTATION(#114021,#114064);
#114021=PRODUCT_DEFINITION_SHAPE('',$,#114084);
#114064=SHAPE_REPRESENTATION('',(#63188),#113978);
#114070=PRODUCT_DEFINITION_CONTEXT('part definition',#114129,'design');
#114084=PRODUCT_DEFINITION('2026-10-05-09-52-00-488',
'ISO 4026 - M2 x 2 - 45H (Pinion Set Screw)',#114103,#114070);
#114103=PRODUCT_DEFINITION_FORMATION('',$,#114144);
#114129=APPLICATION_CONTEXT(
'Core Data for Automotive Mechanical Design Process');
#114130=PRODUCT_CONTEXT('part definition',#114129,'mechanical');
#114144=PRODUCT('2026-10-05-09-52-00-488',
'ISO 4026 - M2 x 2 - 45H (Pinion Set Screw)',$,(#114130));
#114311=COLOUR_RGB('Black',0.12,0.14,0.17);
#114312=FILL_AREA_STYLE_COLOUR('',#114311);
#114313=FILL_AREA_STYLE('',(#114312));
#114314=SURFACE_STYLE_FILL_AREA(#114313);
#114315=SURFACE_SIDE_STYLE('',(#114314));
#114316=SURFACE_STYLE_USAGE(.BOTH.,#114315);
#114317=PRESENTATION_STYLE_ASSIGNMENT((#114316));
ENDSEC;
END-ISO-10303-21;
